ISO-10303-21;
HEADER;
FILE_DESCRIPTION (('STEP AP214'),
    '1' );
FILE_NAME ('Moving Jaw.step',
    '2026-10-09T10:51:02',
    ( '' ),
    ( '' ),
    'SwSTEP 2.0',
    'SolidWorks 2026',
    '' );
FILE_SCHEMA (( 'AUTOMOTIVE_DESIGN' ));
ENDSEC;

DATA;
#8=ORIENTED_EDGE ( 'NONE', *, *, #1064, .F. ) ;
#31=CARTESIAN_POINT ( 'NONE',  ( -56.85751309718151703, 126.2713511641368171, 50.07958431720155090 ) ) ;
#54=VECTOR ( 'NONE', #20690, 999.9999999999998863 ) ;
#66=VECTOR ( 'NONE', #9860, 1000.000000000000114 ) ;
#78=EDGE_CURVE ( 'NONE', #11089, #8677, #1606, .T. ) ;
#89=LINE ( 'NONE', #16195, #5542 ) ;
#91=EDGE_CURVE ( 'NONE', #4221, #20506, #7354, .T. ) ;
#103=DIRECTION ( 'NONE',  ( -7.125109674364536131E-05, 0.9999848031710253382, -0.005512562950849706628 ) ) ;
#108=DIRECTION ( 'NONE',  ( -0.9999164797902015955, 0.000000000000000000, 0.01292414190464162733 ) ) ;
#129=EDGE_LOOP ( 'NONE', ( #6381, #6169 ) ) ;
#132=DIRECTION ( 'NONE',  ( 0.01292394549866738782, 0.005513023399720700692, 0.9999012842304693116 ) ) ;
#143=CARTESIAN_POINT ( 'NONE',  ( -61.67972807482614428, 191.4143309225244707, 257.3032278304543183 ) ) ;
#151=CIRCLE ( 'NONE', #6013, 2.499999999999988010 ) ;
#165=VERTEX_POINT ( 'NONE', #15520 ) ;
#180=DIRECTION ( 'NONE',  ( 0.9999164797902017066, 2.045740421681430110E-15, -0.01292414190464156835 ) ) ;
#191=CARTESIAN_POINT ( 'NONE',  ( 59.65023440614042727, 143.9188730675116688, 165.9879953250834603 ) ) ;
#194=ORIENTED_EDGE ( 'NONE', *, *, #13859, .T. ) ;
#196=CARTESIAN_POINT ( 'NONE',  ( 45.44350069997184249, 168.6907664596096765, 34.02200722522287180 ) ) ;
#200=ORIENTED_EDGE ( 'NONE', *, *, #18910, .T. ) ;
#225=EDGE_LOOP ( 'NONE', ( #13563, #14195, #15245 ) ) ;
#248=ORIENTED_EDGE ( 'NONE', *, *, #8242, .F. ) ;
#252=CARTESIAN_POINT ( 'NONE',  ( 11.11764968563295142, 180.4772689128618879, 86.40582449793498654 ) ) ;
#275=ADVANCED_FACE ( 'NONE', ( #19418 ), #17495, .F. ) ;
#287=( NAMED_UNIT ( * ) SI_UNIT ( $, .STERADIAN. ) SOLID_ANGLE_UNIT ( ) );
#301=EDGE_LOOP ( 'NONE', ( #15173, #17120, #19580, #5311 ) ) ;
#341=DIRECTION ( 'NONE',  ( 0.01292394549866738782, 0.005513023399720700692, 0.9999012842304693116 ) ) ;
#373=CARTESIAN_POINT ( 'NONE',  ( 50.34271970654513950, 126.1473081376433214, 26.19246016726700788 ) ) ;
#377=CYLINDRICAL_SURFACE ( 'NONE', #4764, 2.499999999999988010 ) ;
#380=EDGE_CURVE ( 'NONE', #16237, #5742, #16043, .T. ) ;
#404=CYLINDRICAL_SURFACE ( 'NONE', #18670, 2.499999999999988010 ) ;
#452=EDGE_CURVE ( 'NONE', #165, #13755, #9315, .T. ) ;
#454=ORIENTED_EDGE ( 'NONE', *, *, #13601, .T. ) ;
#478=LINE ( 'NONE', #14400, #9234 ) ;
#483=ORIENTED_EDGE ( 'NONE', *, *, #78, .T. ) ;
#484=LINE ( 'NONE', #12774, #13961 ) ;
#502=VECTOR ( 'NONE', #7954, 1000.000000000000114 ) ;
#506=ORIENTED_EDGE ( 'NONE', *, *, #4777, .T. ) ;
#512=CARTESIAN_POINT ( 'NONE',  ( -56.88982296092818558, 126.2575686056375304, 47.57983110662539161 ) ) ;
#513=LINE ( 'NONE', #7857, #9305 ) ;
#528=AXIS2_PLACEMENT_3D ( 'NONE', #18973, #11647, #20466 ) ;
#530=VERTEX_POINT ( 'NONE', #20541 ) ;
#560=FACE_OUTER_BOUND ( 'NONE', #1569, .T. ) ;
#569=EDGE_CURVE ( 'NONE', #11631, #5077, #22232, .T. ) ;
#621=ORIENTED_EDGE ( 'NONE', *, *, #19931, .T. ) ;
#635=ORIENTED_EDGE ( 'NONE', *, *, #11447, .F. ) ;
#656=EDGE_CURVE ( 'NONE', #4221, #1058, #10790, .T. ) ;
#666=EDGE_CURVE ( 'NONE', #5961, #15373, #15750, .T. ) ;
#670=ADVANCED_FACE ( 'NONE', ( #21226 ), #1950, .F. ) ;
#676=EDGE_CURVE ( 'NONE', #9640, #15200, #1828, .T. ) ;
#681=FACE_OUTER_BOUND ( 'NONE', #15154, .T. ) ;
#682=EDGE_CURVE ( 'NONE', #18467, #17658, #151, .T. ) ;
#683=FACE_OUTER_BOUND ( 'NONE', #19348, .T. ) ;
#715=DIRECTION ( 'NONE',  ( -0.01292394549866632963, -0.005513023399716958026, -0.9999012842304692006 ) ) ;
#743=EDGE_CURVE ( 'NONE', #6677, #18381, #9176, .T. ) ;
#753=CARTESIAN_POINT ( 'NONE',  ( 11.11871845208410825, 165.4774968652965299, 86.48851294219772967 ) ) ;
#757=ORIENTED_EDGE ( 'NONE', *, *, #682, .F. ) ;
#761=DIRECTION ( 'NONE',  ( -0.9999164797902015955, 0.000000000000000000, 0.01292414190464162733 ) ) ;
#763=AXIS2_PLACEMENT_3D ( 'NONE', #20757, #10102, #22458 ) ;
#765=CONICAL_SURFACE ( 'NONE', #22367, 2.499999999999988010, 1.029744258676651425 ) ;
#773=DIRECTION ( 'NONE',  ( 7.125109674364536131E-05, -0.9999848031710253382, 0.005512562950849705760 ) ) ;
#780=ORIENTED_EDGE ( 'NONE', *, *, #380, .T. ) ;
#789=CARTESIAN_POINT ( 'NONE',  ( 53.31522717123864652, 127.4153035195790835, 256.1697555402749913 ) ) ;
#791=CARTESIAN_POINT ( 'NONE',  ( 21.11966452740471212, 140.4778767860209143, 86.49708559692255960 ) ) ;
#796=CARTESIAN_POINT ( 'NONE',  ( 58.06705108255369652, 143.2435277010459060, 43.50008800685101562 ) ) ;
#798=EDGE_CURVE ( 'NONE', #12751, #4221, #9395, .T. ) ;
#841=VECTOR ( 'NONE', #4617, 1000.000000000000114 ) ;
#844=CARTESIAN_POINT ( 'NONE',  ( 59.65144567478507298, 126.9191314136042479, 166.0817088952479139 ) ) ;
#845=ORIENTED_EDGE ( 'NONE', *, *, #7582, .F. ) ;
#855=CIRCLE ( 'NONE', #14444, 3.399999999999986144 ) ;
#868=CLOSED_SHELL ( 'NONE', ( #9507, #3329, #670, #6159, #20217, #3581, #16558, #8125, #4845, #18892, #6672, #22153, #20922, #4844, #14910, #4014, #5202, #929, #275, #10956, #17213, #7692, #12682, #11010, #12614, #8148, #7028, #18141, #11464, #12732, #13758, #18689, #18451, #13047, #17407, #9935, #7990, #22077, #9907, #19849, #10891, #1767, #2351, #5694, #9049, #9933, #7246, #15717, #5307, #20059, #20447, #4217, #17804, #17486, #1253, #13446, #10638, #13478 ) ) ;
#876=ORIENTED_EDGE ( 'NONE', *, *, #13601, .F. ) ;
#877=DIRECTION ( 'NONE',  ( 0.9999164797902015955, 0.000000000000000000, -0.01292414190463754553 ) ) ;
#900=CARTESIAN_POINT ( 'NONE',  ( 1.833149449381782370, 126.7813058286111101, 141.8273149490030391 ) ) ;
#901=ORIENTED_EDGE ( 'NONE', *, *, #13633, .F. ) ;
#904=VECTOR ( 'NONE', #2432, 1000.000000000000114 ) ;
#909=VECTOR ( 'NONE', #4331, 999.9999999999998863 ) ;
#919=DIRECTION ( 'NONE',  ( -0.8637520339192008567, -0.002839416958727990648, -0.5039090806998601790 ) ) ;
#925=AXIS2_PLACEMENT_3D ( 'NONE', #14066, #8982, #17618 ) ;
#929=ADVANCED_FACE ( 'NONE', ( #681 ), #17534, .F. ) ;
#945=ORIENTED_EDGE ( 'NONE', *, *, #10075, .T. ) ;
#967=CYLINDRICAL_SURFACE ( 'NONE', #6913, 2.499999999999988010 ) ;
#1003=ORIENTED_EDGE ( 'NONE', *, *, #14860, .T. ) ;
#1021=LINE ( 'NONE', #20304, #66 ) ;
#1042=CIRCLE ( 'NONE', #21914, 3.399999999999986144 ) ;
#1058=VERTEX_POINT ( 'NONE', #22289 ) ;
#1063=CARTESIAN_POINT ( 'NONE',  ( 68.31397436809166379, 127.4153035195791119, 255.9758934117053570 ) ) ;
#1064=EDGE_CURVE ( 'NONE', #15597, #5961, #10038, .T. ) ;
#1072=DIRECTION ( 'NONE',  ( 0.9999164797902015955, 2.045145117964614424E-15, -0.01292414190464167591 ) ) ;
#1074=CIRCLE ( 'NONE', #21586, 2.499999999999988010 ) ;
#1087=LINE ( 'NONE', #22190, #15813 ) ;
#1103=EDGE_CURVE ( 'NONE', #3194, #20616, #20810, .T. ) ;
#1110=DIRECTION ( 'NONE',  ( 7.125109674364534776E-05, -0.9999848031710252272, 0.005512562950849704893 ) ) ;
#1126=ORIENTED_EDGE ( 'NONE', *, *, #6817, .T. ) ;
#1136=CARTESIAN_POINT ( 'NONE',  ( 58.09936094630035797, 143.2573102595451928, 45.99984121742717491 ) ) ;
#1142=CARTESIAN_POINT ( 'NONE',  ( 42.33134245603051937, 168.8134312302534283, 56.31375288182659489 ) ) ;
#1153=ORIENTED_EDGE ( 'NONE', *, *, #13766, .T. ) ;
#1182=VECTOR ( 'NONE', #13570, 999.9999999999998863 ) ;
#1235=DIRECTION ( 'NONE',  ( 0.9999164797902015955, 2.044556590511377167E-15, -0.01292414190464178346 ) ) ;
#1237=CARTESIAN_POINT ( 'NONE',  ( -41.67747345744867715, 165.9786531560170033, 257.1849355913340673 ) ) ;
#1243=VERTEX_POINT ( 'NONE', #16467 ) ;
#1249=VECTOR ( 'NONE', #6127, 999.9999999999998863 ) ;
#1253=ADVANCED_FACE ( 'NONE', ( #21809 ), #9052, .F. ) ;
#1298=CARTESIAN_POINT ( 'NONE',  ( 48.31072223536619958, 166.8507685304810764, 256.0170097695137201 ) ) ;
#1300=CARTESIAN_POINT ( 'NONE',  ( 1.833149449381782370, 126.7813058286111101, 141.8273149490030391 ) ) ;
#1306=EDGE_LOOP ( 'NONE', ( #12089, #16174 ) ) ;
#1311=CARTESIAN_POINT ( 'NONE',  ( 58.90831880861169623, 126.6021325681202825, 108.5873850519959092 ) ) ;
#1312=DIRECTION ( 'NONE',  ( -0.01292394549866632963, -0.005513023399716958026, -0.9999012842304692006 ) ) ;
#1314=CARTESIAN_POINT ( 'NONE',  ( -44.26142469380095434, 168.8134312302532862, 57.43298357076854899 ) ) ;
#1320=DIRECTION ( 'NONE',  ( -0.01292394549866632963, -0.005513023399716958026, -0.9999012842304692006 ) ) ;
#1321=DIRECTION ( 'NONE',  ( 0.9999164797902017066, 0.000000000000000000, -0.01292414190463751951 ) ) ;
#1335=CARTESIAN_POINT ( 'NONE',  ( 48.02316444802085016, 166.7281037598372961, 233.7692061953857774 ) ) ;
#1360=CARTESIAN_POINT ( 'NONE',  ( 45.44350069997184249, 168.6907664596096765, 34.02200722522287180 ) ) ;
#1377=EDGE_CURVE ( 'NONE', #22319, #11631, #22483, .T. ) ;
#1387=EDGE_CURVE ( 'NONE', #16056, #3377, #16085, .T. ) ;
#1395=DIRECTION ( 'NONE',  ( 1.000000000000000000, 0.000000000000000000, 0.000000000000000000 ) ) ;
#1396=LINE ( 'NONE', #6454, #3814 ) ;
#1397=DIRECTION ( 'NONE',  ( -0.9999164797902015955, 0.000000000000000000, 0.01292414190464162733 ) ) ;
#1408=CONICAL_SURFACE ( 'NONE', #5410, 2.499999999999988010, 1.029744258676651425 ) ;
#1411=ORIENTED_EDGE ( 'NONE', *, *, #19388, .F. ) ;
#1414=EDGE_CURVE ( 'NONE', #3247, #10313, #19707, .T. ) ;
#1418=ORIENTED_EDGE ( 'NONE', *, *, #21040, .T. ) ;
#1434=CARTESIAN_POINT ( 'NONE',  ( -56.11438623100815448, 126.5883500096207683, 107.5739081604535414 ) ) ;
#1452=CYLINDRICAL_SURFACE ( 'NONE', #9723, 3.399999999999986144 ) ;
#1482=CIRCLE ( 'NONE', #4394, 2.499999999999988010 ) ;
#1484=DIRECTION ( 'NONE',  ( -0.01292394549866632963, -0.005513023399716958026, -0.9999012842304692006 ) ) ;
#1491=EDGE_CURVE ( 'NONE', #19968, #18675, #13691, .T. ) ;
#1495=LINE ( 'NONE', #6987, #15156 ) ;
#1497=DIRECTION ( 'NONE',  ( -0.01292394549866632963, -0.005513023399716958026, -0.9999012842304692006 ) ) ;
#1511=CARTESIAN_POINT ( 'NONE',  ( -41.96503124479402658, 165.8559883853732515, 234.9371320172060678 ) ) ;
#1525=DIRECTION ( 'NONE',  ( 7.125109674364536131E-05, -0.9999848031710253382, 0.005512562950849705760 ) ) ;
#1559=CARTESIAN_POINT ( 'NONE',  ( 58.87600894486503478, 126.5883500096209815, 106.0876318414197499 ) ) ;
#1569=EDGE_LOOP ( 'NONE', ( #12182, #20918, #6623 ) ) ;
#1582=ORIENTED_EDGE ( 'NONE', *, *, #10898, .F. ) ;
#1587=EDGE_LOOP ( 'NONE', ( #2535, #7607 ) ) ;
#1597=CARTESIAN_POINT ( 'NONE',  ( -49.64993871177497198, 140.1470898690141098, 27.40669857513504226 ) ) ;
#1606=LINE ( 'NONE', #15865, #11517 ) ;
#1608=FACE_OUTER_BOUND ( 'NONE', #14068, .T. ) ;
#1614=VERTEX_POINT ( 'NONE', #5267 ) ;
#1633=EDGE_LOOP ( 'NONE', ( #20805, #14604, #13579, #1411 ) ) ;
#1653=VERTEX_POINT ( 'NONE', #14382 ) ;
#1666=UNCERTAINTY_MEASURE_WITH_UNIT (LENGTH_MEASURE( 1.000000000000000082E-05 ), #7282, 'distance_accuracy_value', 'NONE');
#1670=CARTESIAN_POINT ( 'NONE',  ( 50.34270678259964882, 126.1473026246199254, 26.19146026598277643 ) ) ;
#1696=ORIENTED_EDGE ( 'NONE', *, *, #16280, .F. ) ;
#1716=EDGE_CURVE ( 'NONE', #20174, #6772, #18260, .T. ) ;
#1717=CARTESIAN_POINT ( 'NONE',  ( -56.14669609475481593, 126.5745674511214673, 105.0741549498773679 ) ) ;
#1719=DIRECTION ( 'NONE',  ( 0.9999164797902015955, 0.000000000000000000, -0.01292414190463754553 ) ) ;
#1732=ORIENTED_EDGE ( 'NONE', *, *, #3168, .F. ) ;
#1758=LINE ( 'NONE', #31, #17434 ) ;
#1767=ADVANCED_FACE ( 'NONE', ( #19961 ), #10909, .F. ) ;
#1796=CARTESIAN_POINT ( 'NONE',  ( 58.84369908111836622, 126.5745674511216947, 103.5878786308435906 ) ) ;
#1828=LINE ( 'NONE', #5486, #10054 ) ;
#1836=MANIFOLD_SOLID_BREP ( 'Boss-Extrude1', #868 ) ;
#1837=ORIENTED_EDGE ( 'NONE', *, *, #5709, .F. ) ;
#1856=PRODUCT_DEFINITION_FORMATION_WITH_SPECIFIED_SOURCE ( 'ANY', '', #16535, .NOT_KNOWN. ) ;
#1858=DIRECTION ( 'NONE',  ( 7.125109674364534776E-05, -0.9999848031710252272, 0.005512562950849704893 ) ) ;
#1866=ORIENTED_EDGE ( 'NONE', *, *, #21450, .T. ) ;
#1881=UNCERTAINTY_MEASURE_WITH_UNIT (LENGTH_MEASURE( 1.000000000000000082E-05 ), #12716, 'distance_accuracy_value', 'NONE');
#1886=DIRECTION ( 'NONE',  ( 0.9999164797902017066, 2.045740421681430110E-15, -0.01292414190464156835 ) ) ;
#1895=VECTOR ( 'NONE', #20236, 999.9999999999998863 ) ;
#1901=EDGE_CURVE ( 'NONE', #4209, #1243, #18281, .T. ) ;
#1914=FILL_AREA_STYLE_COLOUR ( '', #15733 ) ;
#1930=VERTEX_POINT ( 'NONE', #16741 ) ;
#1950=CYLINDRICAL_SURFACE ( 'NONE', #17036, 2.499999999999988010 ) ;
#1952=EDGE_CURVE ( 'NONE', #18558, #11233, #1042, .T. ) ;
#1962=EDGE_LOOP ( 'NONE', ( #14254, #780, #7957, #4938 ) ) ;
#1985=DIRECTION ( 'NONE',  ( -0.01292394549866738782, -0.005513023399720700692, -0.9999012842304693116 ) ) ;
#1986=CIRCLE ( 'NONE', #14841, 3.399999999999992806 ) ;
#2005=DIRECTION ( 'NONE',  ( -0.8504393858994485633, 0.002839416958724588855, 0.5260653843604455870 ) ) ;
#2038=CARTESIAN_POINT ( 'NONE',  ( -55.34026779967800280, 145.4210017871401703, 167.4659909391495773 ) ) ;
#2052=DIRECTION ( 'NONE',  ( 7.125109674364536131E-05, -0.9999848031710253382, 0.005512562950849705760 ) ) ;
#2059=DIRECTION ( 'NONE',  ( -0.01292394549866632963, -0.005513023399716958026, -0.9999012842304692006 ) ) ;
#2088=VERTEX_POINT ( 'NONE', #22628 ) ;
#2093=CARTESIAN_POINT ( 'NONE',  ( 65.34011313256004883, 145.1470193978928478, 25.89385934263130196 ) ) ;
#2105=EDGE_CURVE ( 'NONE', #3748, #11233, #10394, .T. ) ;
#2129=SURFACE_STYLE_USAGE ( .BOTH. , #7189 ) ;
#2162=ORIENTED_EDGE ( 'NONE', *, *, #16280, .T. ) ;
#2228=CARTESIAN_POINT ( 'NONE',  ( -56.11559749965279309, 143.5880916635282176, 107.4801945902891021 ) ) ;
#2246=DIRECTION ( 'NONE',  ( -0.01292394549866738608, -0.005513023399720699824, -0.9999012842304692006 ) ) ;
#2248=DIRECTION ( 'NONE',  ( 0.01292394549866738782, 0.005513023399720700692, 0.9999012842304693116 ) ) ;
#2279=CIRCLE ( 'NONE', #20958, 3.399999999999992806 ) ;
#2289=CONICAL_SURFACE ( 'NONE', #22071, 3.399999999999986144, 1.029744258676653201 ) ;
#2290=EDGE_LOOP ( 'NONE', ( #13159, #19316, #9264 ) ) ;
#2292=LINE ( 'NONE', #12527, #5273 ) ;
#2300=DIRECTION ( 'NONE',  ( 7.125109674364534776E-05, -0.9999848031710252272, 0.005512562950849704893 ) ) ;
#2304=CONICAL_SURFACE ( 'NONE', #18102, 2.499999999999988010, 1.029744258676651425 ) ;
#2321=CARTESIAN_POINT ( 'NONE',  ( 65.34111304903984774, 145.1470193978928478, 25.89384641848939239 ) ) ;
#2341=EDGE_CURVE ( 'NONE', #19120, #4209, #20450, .T. ) ;
#2351=ADVANCED_FACE ( 'NONE', ( #22051 ), #8290, .F. ) ;
#2362=DIRECTION ( 'NONE',  ( 0.01292394549866738608, 0.005513023399720699824, 0.9999012842304692006 ) ) ;
#2376=DIRECTION ( 'NONE',  ( -0.9999164797902017066, -2.045740421681430110E-15, 0.01292414190464156835 ) ) ;
#2384=EDGE_CURVE ( 'NONE', #11720, #5047, #13476, .T. ) ;
#2403=DIRECTION ( 'NONE',  ( 0.9999164797902015955, 0.000000000000000000, -0.01292414190463754553 ) ) ;
#2422=EDGE_CURVE ( 'NONE', #12381, #19968, #5049, .T. ) ;
#2430=DIRECTION ( 'NONE',  ( 0.01292394549866738782, 0.005513023399720700692, 0.9999012842304693116 ) ) ;
#2432=DIRECTION ( 'NONE',  ( 0.01292394549866738608, 0.005513023399720698957, 0.9999012842304692006 ) ) ;
#2505=ORIENTED_EDGE ( 'NONE', *, *, #6817, .F. ) ;
#2535=ORIENTED_EDGE ( 'NONE', *, *, #3979, .F. ) ;
#2564=AXIS2_PLACEMENT_3D ( 'NONE', #13742, #1110, #10281 ) ;
#2567=FACE_OUTER_BOUND ( 'NONE', #10625, .T. ) ;
#2638=EDGE_CURVE ( 'NONE', #11335, #12812, #9124, .T. ) ;
#2649=EDGE_CURVE ( 'NONE', #12751, #1058, #13221, .T. ) ;
#2654=EDGE_CURVE ( 'NONE', #18220, #6772, #13448, .T. ) ;
#2663=EDGE_LOOP ( 'NONE', ( #17888, #15453, #9725, #10215 ) ) ;
#2695=CARTESIAN_POINT ( 'NONE',  ( 65.44029839719591735, 190.1904397277867531, 33.64500428368677376 ) ) ;
#2705=CARTESIAN_POINT ( 'NONE',  ( 59.68254426988709582, 143.9326556260109555, 168.4877485356596196 ) ) ;
#2715=AXIS2_PLACEMENT_3D ( 'NONE', #10584, #1858, #15899 ) ;
#2741=DIRECTION ( 'NONE',  ( 0.01292394549866760292, 0.005513023399720701559, 0.9999012842304693116 ) ) ;
#2795=CARTESIAN_POINT ( 'NONE',  ( 59.65023440614042727, 143.9188730675116688, 165.9879953250834603 ) ) ;
#2797=DIRECTION ( 'NONE',  ( 7.125109674364534776E-05, -0.9999848031710252272, 0.005512562950849704893 ) ) ;
#2803=LINE ( 'NONE', #7743, #16222 ) ;
#2833=CARTESIAN_POINT ( 'NONE',  ( -38.27775742616200461, 165.9786531560170033, 257.1409935088582870 ) ) ;
#2843=PLANE ( 'NONE',  #19899 ) ;
#2851=DIRECTION ( 'NONE',  ( 7.125109674364534776E-05, -0.9999848031710252272, 0.005512562950849704893 ) ) ;
#2862=ORIENTED_EDGE ( 'NONE', *, *, #19183, .F. ) ;
#2897=DIRECTION ( 'NONE',  ( -0.01292394549866632963, -0.005513023399716958026, -0.9999012842304692006 ) ) ;
#2920=AXIS2_PLACEMENT_3D ( 'NONE', #22344, #6190, #1484 ) ;
#2966=AXIS2_PLACEMENT_3D ( 'NONE', #14015, #8695, #7325 ) ;
#2980=LINE ( 'NONE', #17466, #21358 ) ;
#2987=ORIENTED_EDGE ( 'NONE', *, *, #11212, .T. ) ;
#3004=ORIENTED_EDGE ( 'NONE', *, *, #20722, .T. ) ;
#3016=ORIENTED_EDGE ( 'NONE', *, *, #743, .F. ) ;
#3049=DIRECTION ( 'NONE',  ( 0.9999164797902015955, 0.000000000000000000, -0.01292414190463754553 ) ) ;
#3073=DIRECTION ( 'NONE',  ( 0.9999164797902015955, 2.045733645417851681E-15, -0.01292414190464156835 ) ) ;
#3102=CARTESIAN_POINT ( 'NONE',  ( 0.000000000000000000, 0.000000000000000000, 0.000000000000000000 ) ) ;
#3105=CARTESIAN_POINT ( 'NONE',  ( 45.73105848731719192, 168.8134312302534283, 56.26981079935081453 ) ) ;
#3108=PLANE ( 'NONE',  #20633 ) ;
#3111=DIRECTION ( 'NONE',  ( -0.9999164797902015955, 0.000000000000000000, 0.01292414190464162733 ) ) ;
#3132=DIRECTION ( 'NONE',  ( 0.01292394549866738782, 0.005513023399720700692, 0.9999012842304693116 ) ) ;
#3154=DIRECTION ( 'NONE',  ( -0.9999164797902015955, 0.000000000000000000, 0.01292414190464162733 ) ) ;
#3157=ORIENTED_EDGE ( 'NONE', *, *, #9476, .F. ) ;
#3164=EDGE_CURVE ( 'NONE', #13257, #15597, #21565, .T. ) ;
#3168=EDGE_CURVE ( 'NONE', #11414, #11720, #12870, .T. ) ;
#3172=EDGE_CURVE ( 'NONE', #12249, #8826, #8048, .T. ) ;
#3182=CARTESIAN_POINT ( 'NONE',  ( -44.54898248114630377, 168.6907664596094776, 35.18517999664061335 ) ) ;
#3186=AXIS2_PLACEMENT_3D ( 'NONE', #4220, #14597, #11136 ) ;
#3190=LINE ( 'NONE', #10447, #3750 ) ;
#3194=VERTEX_POINT ( 'NONE', #7686 ) ;
#3195=CARTESIAN_POINT ( 'NONE',  ( -56.89103422957282419, 143.2573102595449654, 47.48611753646095224 ) ) ;
#3198=EDGE_CURVE ( 'NONE', #21215, #530, #19771, .T. ) ;
#3213=ORIENTED_EDGE ( 'NONE', *, *, #22107, .T. ) ;
#3214=AXIS2_PLACEMENT_3D ( 'NONE', #20557, #18848, #3111 ) ;
#3219=VERTEX_POINT ( 'NONE', #18265 ) ;
#3237=CARTESIAN_POINT ( 'NONE',  ( 44.91100620407951993, 166.8507685304810764, 256.0609518519894436 ) ) ;
#3247=VERTEX_POINT ( 'NONE', #8021 ) ;
#3271=PRODUCT_DEFINITION_CONTEXT ( 'detailed design', #8949, 'design' ) ;
#3302=AXIS2_PLACEMENT_3D ( 'NONE', #8699, #12305, #9041 ) ;
#3303=FACE_OUTER_BOUND ( 'NONE', #6567, .T. ) ;
#3329=ADVANCED_FACE ( 'NONE', ( #15053 ), #10302, .F. ) ;
#3356=FACE_OUTER_BOUND ( 'NONE', #17498, .T. ) ;
#3377=VERTEX_POINT ( 'NONE', #20758 ) ;
#3381=DIRECTION ( 'NONE',  ( -0.01292394549866632963, -0.005513023399716958026, -0.9999012842304692006 ) ) ;
#3392=( NAMED_UNIT ( * ) PLANE_ANGLE_UNIT ( ) SI_UNIT ( $, .RADIAN. ) );
#3405=AXIS2_PLACEMENT_3D ( 'NONE', #1360, #15380, #22328 ) ;
#3452=CIRCLE ( 'NONE', #528, 2.499999999999988010 ) ;
#3458=VECTOR ( 'NONE', #5783, 1000.000000000000000 ) ;
#3471=CYLINDRICAL_SURFACE ( 'NONE', #2715, 2.499999999999988010 ) ;
#3484=DIRECTION ( 'NONE',  ( 7.125109674364534776E-05, -0.9999848031710252272, 0.005512562950849704893 ) ) ;
#3491=EDGE_CURVE ( 'NONE', #20616, #13170, #7315, .T. ) ;
#3499=DIRECTION ( 'NONE',  ( 7.125109674364534776E-05, -0.9999848031710252272, 0.005512562950849704893 ) ) ;
#3512=AXIS2_PLACEMENT_3D ( 'NONE', #252, #14273, #4949 ) ;
#3536=DIRECTION ( 'NONE',  ( 7.125109674364534776E-05, -0.9999848031710252272, 0.005512562950849704893 ) ) ;
#3548=CARTESIAN_POINT ( 'NONE',  ( 58.09936094630035797, 143.2573102595451928, 45.99984121742717491 ) ) ;
#3556=DIRECTION ( 'NONE',  ( 7.125109674364534776E-05, -0.9999848031710252272, 0.005512562950849704893 ) ) ;
#3559=VECTOR ( 'NONE', #3132, 999.9999999999998863 ) ;
#3577=LINE ( 'NONE', #2093, #20315 ) ;
#3581=ADVANCED_FACE ( 'NONE', ( #560 ), #1408, .F. ) ;
#3613=EDGE_LOOP ( 'NONE', ( #6256, #194, #9915, #11286 ) ) ;
#3617=VECTOR ( 'NONE', #8185, 1000.000000000000114 ) ;
#3644=AXIS2_PLACEMENT_3D ( 'NONE', #7146, #15360, #20610 ) ;
#3646=CYLINDRICAL_SURFACE ( 'NONE', #18442, 3.399999999999992806 ) ;
#3676=VERTEX_POINT ( 'NONE', #6222 ) ;
#3693=ORIENTED_EDGE ( 'NONE', *, *, #2384, .T. ) ;
#3715=CARTESIAN_POINT ( 'NONE',  ( -41.67747345744867715, 165.9786531560170033, 257.1849355913340673 ) ) ;
#3748=VERTEX_POINT ( 'NONE', #9791 ) ;
#3750=VECTOR ( 'NONE', #11841, 999.9999999999998863 ) ;
#3769=AXIS2_PLACEMENT_3D ( 'NONE', #6347, #13696, #11966 ) ;
#3814=VECTOR ( 'NONE', #13690, 1000.000000000000000 ) ;
#3822=EDGE_CURVE ( 'NONE', #1653, #16867, #6535, .T. ) ;
#3827=CARTESIAN_POINT ( 'NONE',  ( 58.10057221494500368, 126.2575686056377435, 46.09355478759161429 ) ) ;
#3846=DIRECTION ( 'NONE',  ( 7.125109674364534776E-05, -0.9999848031710252272, 0.005512562950849704893 ) ) ;
#3849=CARTESIAN_POINT ( 'NONE',  ( -16.67992392942989710, 141.4150907639733248, 256.9972695922879780 ) ) ;
#3853=ORIENTED_EDGE ( 'NONE', *, *, #2422, .T. ) ;
#3861=CARTESIAN_POINT ( 'NONE',  ( -16.67992392942989710, 141.4150907639733248, 256.9972695922879780 ) ) ;
#3869=EDGE_LOOP ( 'NONE', ( #14299, #3213, #506 ) ) ;
#3884=CARTESIAN_POINT ( 'NONE',  ( -56.11570452959804101, 145.0902203831569466, 107.4719138853213991 ) ) ;
#3909=DIRECTION ( 'NONE',  ( 0.01292394549866738608, 0.005513023399720698957, 0.9999012842304692006 ) ) ;
#3923=EDGE_LOOP ( 'NONE', ( #16079, #13807, #18487, #11398, #15466, #9182, #3853, #7722, #17575, #5613 ) ) ;
#3929=VECTOR ( 'NONE', #19088, 999.9999999999998863 ) ;
#3951=DIRECTION ( 'NONE',  ( 7.125109674364534776E-05, -0.9999848031710252272, 0.005512562950849704893 ) ) ;
#3952=( NAMED_UNIT ( * ) SI_UNIT ( $, .STERADIAN. ) SOLID_ANGLE_UNIT ( ) );
#3966=AXIS2_PLACEMENT_3D ( 'NONE', #15003, #2362, #21955 ) ;
#3971=VECTOR ( 'NONE', #2005, 1000.000000000000000 ) ;
#3973=ORIENTED_EDGE ( 'NONE', *, *, #18882, .F. ) ;
#3978=CIRCLE ( 'NONE', #18301, 3.399999999999986144 ) ;
#3979=EDGE_CURVE ( 'NONE', #1930, #1614, #16828, .T. ) ;
#3985=DIRECTION ( 'NONE',  ( -0.01104128644981183967, -0.5197558313507629757, -0.8542435049623791077 ) ) ;
#3995=ORIENTED_EDGE ( 'NONE', *, *, #10783, .T. ) ;
#4007=EDGE_LOOP ( 'NONE', ( #16383, #13424 ) ) ;
#4014=ADVANCED_FACE ( 'NONE', ( #9819 ), #10214, .F. ) ;
#4018=ORIENTED_EDGE ( 'NONE', *, *, #20003, .F. ) ;
#4019=DIRECTION ( 'NONE',  ( -0.8637520339192008567, -0.002839416958727990648, -0.5039090806998601790 ) ) ;
#4061=FACE_OUTER_BOUND ( 'NONE', #17532, .T. ) ;
#4062=AXIS2_PLACEMENT_3D ( 'NONE', #1434, #12837, #17065 ) ;
#4068=VECTOR ( 'NONE', #20649, 999.9999999999998863 ) ;
#4099=AXIS2_PLACEMENT_3D ( 'NONE', #10976, #2246, #761 ) ;
#4103=LINE ( 'NONE', #5947, #13948 ) ;
#4113=ORIENTED_EDGE ( 'NONE', *, *, #17200, .T. ) ;
#4118=DIRECTION ( 'NONE',  ( 0.9999164797902015955, 2.045145117964614424E-15, -0.01292414190464167591 ) ) ;
#4125=EDGE_CURVE ( 'NONE', #4299, #6677, #4288, .T. ) ;
#4145=DIRECTION ( 'NONE',  ( -0.01292394549866749710, -0.005513023399720701559, -0.9999012842304693116 ) ) ;
#4149=EDGE_CURVE ( 'NONE', #2088, #20616, #18313, .T. ) ;
#4162=EDGE_CURVE ( 'NONE', #8677, #19674, #8360, .T. ) ;
#4195=ORIENTED_EDGE ( 'NONE', *, *, #4444, .F. ) ;
#4204=FACE_BOUND ( 'NONE', #14450, .T. ) ;
#4206=EDGE_CURVE ( 'NONE', #4699, #15373, #9491, .T. ) ;
#4209=VERTEX_POINT ( 'NONE', #18098 ) ;
#4217=ADVANCED_FACE ( 'NONE', ( #9342 ), #967, .F. ) ;
#4220=CARTESIAN_POINT ( 'NONE',  ( -44.26142469380095434, 168.8134312302532862, 57.43298357076854899 ) ) ;
#4221=VERTEX_POINT ( 'NONE', #18205 ) ;
#4272=EDGE_CURVE ( 'NONE', #20174, #17225, #9803, .T. ) ;
#4285=CARTESIAN_POINT ( 'NONE',  ( -45.07718948873534970, 165.9786531560170033, 257.2288776738097908 ) ) ;
#4288=LINE ( 'NONE', #2705, #21209 ) ;
#4299=VERTEX_POINT ( 'NONE', #15552 ) ;
#4324=AXIS2_PLACEMENT_3D ( 'NONE', #19787, #16734, #877 ) ;
#4331=DIRECTION ( 'NONE',  ( -0.01292394549866738782, -0.005513023399720700692, -0.9999012842304693116 ) ) ;
#4383=DIRECTION ( 'NONE',  ( -0.01292394549866632963, -0.005513023399716958026, -0.9999012842304692006 ) ) ;
#4394=AXIS2_PLACEMENT_3D ( 'NONE', #15938, #12472, #15815 ) ;
#4401=DIRECTION ( 'NONE',  ( -0.9999164797902015955, -2.045733645417851681E-15, 0.01292414190464156835 ) ) ;
#4416=ORIENTED_EDGE ( 'NONE', *, *, #15558, .T. ) ;
#4426=DIRECTION ( 'NONE',  ( -7.125109674364536131E-05, 0.9999848031710253382, -0.005512562950849706628 ) ) ;
#4441=DIRECTION ( 'NONE',  ( 0.01292394549866738608, 0.005513023399720699824, 0.9999012842304692006 ) ) ;
#4444=EDGE_CURVE ( 'NONE', #1243, #4209, #1074, .T. ) ;
#4452=EDGE_LOOP ( 'NONE', ( #10417, #6060, #1418, #22286 ) ) ;
#4457=CARTESIAN_POINT ( 'NONE',  ( 65.34146690339817098, 126.1473081376433498, 25.99859803869739139 ) ) ;
#4503=DIRECTION ( 'NONE',  ( 0.01292394549866738608, 0.005513023399720699824, 0.9999012842304692006 ) ) ;
#4511=DIRECTION ( 'NONE',  ( 0.01292394549866738608, 0.005513023399720698957, 0.9999012842304692006 ) ) ;
#4519=VERTEX_POINT ( 'NONE', #20108 ) ;
#4527=ORIENTED_EDGE ( 'NONE', *, *, #13731, .T. ) ;
#4530=DIRECTION ( 'NONE',  ( -0.9999164797902017066, -2.775557561562891351E-15, 0.01292414190464108437 ) ) ;
#4538=DIRECTION ( 'NONE',  ( -0.9999164797902015955, 0.000000000000000000, 0.01292414190464162733 ) ) ;
#4556=FACE_OUTER_BOUND ( 'NONE', #11973, .T. ) ;
#4599=PLANE ( 'NONE',  #3769 ) ;
#4601=ORIENTED_EDGE ( 'NONE', *, *, #10128, .T. ) ;
#4606=ORIENTED_EDGE ( 'NONE', *, *, #4162, .F. ) ;
#4607=DIRECTION ( 'NONE',  ( 0.01111468050521610164, -0.5103046645782707280, 0.8599218645824314722 ) ) ;
#4612=CARTESIAN_POINT ( 'NONE',  ( 59.61913581103840443, 126.9053488551049611, 163.5819556846717546 ) ) ;
#4614=CARTESIAN_POINT ( 'NONE',  ( 11.12049972950270416, 140.4778767860208859, 86.62632701596898244 ) ) ;
#4617=DIRECTION ( 'NONE',  ( -0.01104128644981183967, -0.5197558313507629757, -0.8542435049623791077 ) ) ;
#4624=CARTESIAN_POINT ( 'NONE',  ( -56.14669609475481593, 126.5745674511214673, 105.0741549498773679 ) ) ;
#4638=DIRECTION ( 'NONE',  ( 0.9999164797902015955, 0.000000000000000000, -0.01292414190463754553 ) ) ;
#4643=FACE_OUTER_BOUND ( 'NONE', #18554, .T. ) ;
#4696=CARTESIAN_POINT ( 'NONE',  ( 58.09925391635511005, 144.7594389791739218, 45.99156051245947907 ) ) ;
#4699=VERTEX_POINT ( 'NONE', #791 ) ;
#4746=ORIENTED_EDGE ( 'NONE', *, *, #10972, .F. ) ;
#4764=AXIS2_PLACEMENT_3D ( 'NONE', #844, #5754, #14638 ) ;
#4777=EDGE_CURVE ( 'NONE', #10313, #3247, #3978, .T. ) ;
#4778=CARTESIAN_POINT ( 'NONE',  ( -45.36474727608072044, 165.8559883853732515, 234.9810740996818481 ) ) ;
#4782=CARTESIAN_POINT ( 'NONE',  ( -56.11559749965279309, 143.5880916635282176, 107.4801945902891021 ) ) ;
#4784=VERTEX_POINT ( 'NONE', #2038 ) ;
#4807=CIRCLE ( 'NONE', #10699, 2.499999999999988010 ) ;
#4815=FACE_BOUND ( 'NONE', #13111, .T. ) ;
#4828=LINE ( 'NONE', #13815, #54 ) ;
#4844=ADVANCED_FACE ( 'NONE', ( #5928 ), #9868, .F. ) ;
#4845=ADVANCED_FACE ( 'NONE', ( #10173 ), #404, .F. ) ;
#4849=FACE_OUTER_BOUND ( 'NONE', #16653, .T. ) ;
#4867=CARTESIAN_POINT ( 'NONE',  ( -44.23502202816609241, 168.8246939296723497, 59.47570800643972433 ) ) ;
#4868=CARTESIAN_POINT ( 'NONE',  ( 45.73105848731719192, 168.8134312302534283, 56.26981079935081453 ) ) ;
#4924=ORIENTED_EDGE ( 'NONE', *, *, #16418, .F. ) ;
#4931=DIRECTION ( 'NONE',  ( -0.9999164797902015955, -2.045733645417851287E-15, 0.01292414190464156835 ) ) ;
#4938=ORIENTED_EDGE ( 'NONE', *, *, #11943, .F. ) ;
#4948=DIRECTION ( 'NONE',  ( -0.9999164797902015955, 0.000000000000000000, 0.01292414190464162733 ) ) ;
#4949=DIRECTION ( 'NONE',  ( -0.9999164797902017066, -2.775557561562891351E-15, 0.01292414190464108437 ) ) ;
#4965=VERTEX_POINT ( 'NONE', #18685 ) ;
#4972=CARTESIAN_POINT ( 'NONE',  ( 51.42288047930750139, 166.7281037598372961, 233.7252641129099970 ) ) ;
#5025=DIRECTION ( 'NONE',  ( 0.01292394549866738782, 0.005513023399720700692, 0.9999012842304693116 ) ) ;
#5042=DIRECTION ( 'NONE',  ( -0.9999164797902015955, 0.000000000000000000, 0.01292414190464162733 ) ) ;
#5045=ORIENTED_EDGE ( 'NONE', *, *, #21469, .F. ) ;
#5047=VERTEX_POINT ( 'NONE', #9481 ) ;
#5049=LINE ( 'NONE', #10691, #14658 ) ;
#5063=DIRECTION ( 'NONE',  ( 7.125109674364536131E-05, -0.9999848031710253382, 0.005512562950849706628 ) ) ;
#5077=VERTEX_POINT ( 'NONE', #7543 ) ;
#5087=CARTESIAN_POINT ( 'NONE',  ( -49.64992578782946708, 140.1470953820375200, 27.40769847641930212 ) ) ;
#5121=DIRECTION ( 'NONE',  ( 7.125109674364534776E-05, -0.9999848031710252272, 0.005512562950849704893 ) ) ;
#5155=DIRECTION ( 'NONE',  ( -0.01292394549866632963, -0.005513023399716958026, -0.9999012842304692006 ) ) ;
#5199=ORIENTED_EDGE ( 'NONE', *, *, #12045, .T. ) ;
#5202=ADVANCED_FACE ( 'NONE', ( #17176 ), #9943, .F. ) ;
#5203=CARTESIAN_POINT ( 'NONE',  ( 44.62344841673417761, 166.7281037598372961, 233.8131482778615293 ) ) ;
#5247=DIRECTION ( 'NONE',  ( -0.01292394549866632963, -0.005513023399716958026, -0.9999012842304692006 ) ) ;
#5261=DIRECTION ( 'NONE',  ( 7.125109674364534776E-05, -0.9999848031710252272, 0.005512562950849704893 ) ) ;
#5267=CARTESIAN_POINT ( 'NONE',  ( 48.84321673125851504, 168.6907664596096765, 33.97806514274709144 ) ) ;
#5269=EDGE_CURVE ( 'NONE', #22319, #5077, #484, .T. ) ;
#5273=VECTOR ( 'NONE', #341, 999.9999999999998863 ) ;
#5301=LINE ( 'NONE', #373, #22006 ) ;
#5307=ADVANCED_FACE ( 'NONE', ( #5864 ), #17606, .F. ) ;
#5311=ORIENTED_EDGE ( 'NONE', *, *, #4149, .F. ) ;
#5319=DIRECTION ( 'NONE',  ( -0.01292394549866632963, -0.005513023399716958026, -0.9999012842304692006 ) ) ;
#5320=DIRECTION ( 'NONE',  ( 7.125109674364534776E-05, -0.9999848031710252272, 0.005512562950849704893 ) ) ;
#5323=AXIS2_PLACEMENT_3D ( 'NONE', #12075, #15536, #13907 ) ;
#5399=LINE ( 'NONE', #2321, #8444 ) ;
#5401=PLANE ( 'NONE',  #22486 ) ;
#5410=AXIS2_PLACEMENT_3D ( 'NONE', #5812, #19823, #11126 ) ;
#5447=LINE ( 'NONE', #20963, #9988 ) ;
#5486=CARTESIAN_POINT ( 'NONE',  ( -55.37125936483477773, 126.9053488551047053, 165.0682320037055320 ) ) ;
#5528=CARTESIAN_POINT ( 'NONE',  ( -55.37247063347942344, 143.9050905090121546, 164.9745184335410499 ) ) ;
#5542=VECTOR ( 'NONE', #9141, 1000.000000000000114 ) ;
#5558=ORIENTED_EDGE ( 'NONE', *, *, #17934, .T. ) ;
#5613=ORIENTED_EDGE ( 'NONE', *, *, #4206, .T. ) ;
#5617=PLANE ( 'NONE',  #16249 ) ;
#5632=CIRCLE ( 'NONE', #10403, 3.399999999999986144 ) ;
#5640=VERTEX_POINT ( 'NONE', #11590 ) ;
#5656=LINE ( 'NONE', #19217, #14875 ) ;
#5674=DIRECTION ( 'NONE',  ( -0.01292394549866738608, -0.005513023399720699824, -0.9999012842304692006 ) ) ;
#5694=ADVANCED_FACE ( 'NONE', ( #683 ), #7672, .T. ) ;
#5709=EDGE_CURVE ( 'NONE', #6772, #18256, #22229, .T. ) ;
#5739=LINE ( 'NONE', #5857, #11238 ) ;
#5742=VERTEX_POINT ( 'NONE', #20642 ) ;
#5754=DIRECTION ( 'NONE',  ( 7.125109674364534776E-05, -0.9999848031710252272, 0.005512562950849704893 ) ) ;
#5783=DIRECTION ( 'NONE',  ( -0.8504393858994485633, 0.002839416958724588855, 0.5260653843604455870 ) ) ;
#5812=CARTESIAN_POINT ( 'NONE',  ( -55.34016076973275489, 143.9188730675114414, 167.4742716441172377 ) ) ;
#5823=ORIENTED_EDGE ( 'NONE', *, *, #11174, .F. ) ;
#5834=DIRECTION ( 'NONE',  ( -7.125109674381880655E-05, 0.9999848031710253382, -0.005512562950849702291 ) ) ;
#5840=CARTESIAN_POINT ( 'NONE',  ( -19.00908416305977156, 180.4221386788646271, 76.79453591276953262 ) ) ;
#5857=CARTESIAN_POINT ( 'NONE',  ( 68.30941429790007646, 191.4143309225247549, 255.6230893828509352 ) ) ;
#5861=CARTESIAN_POINT ( 'NONE',  ( -19.00623411919002592, 140.4227465520235967, 77.01503843080352851 ) ) ;
#5864=FACE_OUTER_BOUND ( 'NONE', #14944, .T. ) ;
#5871=FACE_OUTER_BOUND ( 'NONE', #7023, .T. ) ;
#5904=DIRECTION ( 'NONE',  ( -0.9999164797902017066, -2.775557561562891351E-15, 0.01292414190464108437 ) ) ;
#5909=ORIENTED_EDGE ( 'NONE', *, *, #6115, .F. ) ;
#5921=VECTOR ( 'NONE', #19563, 1000.000000000000000 ) ;
#5928=FACE_OUTER_BOUND ( 'NONE', #225, .T. ) ;
#5929=DIRECTION ( 'NONE',  ( -0.01292394549866632963, -0.005513023399716958026, -0.9999012842304692006 ) ) ;
#5931=VECTOR ( 'NONE', #16668, 999.9999999999998863 ) ;
#5934=ORIENTED_EDGE ( 'NONE', *, *, #3491, .T. ) ;
#5947=CARTESIAN_POINT ( 'NONE',  ( -55.30785090598609344, 143.9326556260107282, 169.9740248546933969 ) ) ;
#5961=VERTEX_POINT ( 'NONE', #21639 ) ;
#5965=DIRECTION ( 'NONE',  ( 7.125109674364534776E-05, -0.9999848031710252272, 0.005512562950849704893 ) ) ;
#6013=AXIS2_PLACEMENT_3D ( 'NONE', #20888, #17354, #2059 ) ;
#6026=CARTESIAN_POINT ( 'NONE',  ( 51.71043826665287924, 166.8507685304810764, 255.9730676870379114 ) ) ;
#6027=CARTESIAN_POINT ( 'NONE',  ( -49.64992578782946708, 140.1470953820375200, 27.40769847641928791 ) ) ;
#6060=ORIENTED_EDGE ( 'NONE', *, *, #18021, .T. ) ;
#6073=LINE ( 'NONE', #15048, #909 ) ;
#6091=ORIENTED_EDGE ( 'NONE', *, *, #3164, .T. ) ;
#6115=EDGE_CURVE ( 'NONE', #9640, #3676, #1482, .T. ) ;
#6127=DIRECTION ( 'NONE',  ( -0.01292394549866738782, -0.005513023399720700692, -0.9999012842304693116 ) ) ;
#6159=ADVANCED_FACE ( 'NONE', ( #7060 ), #8801, .F. ) ;
#6169=ORIENTED_EDGE ( 'NONE', *, *, #12819, .F. ) ;
#6178=AXIS2_PLACEMENT_3D ( 'NONE', #4614, #14987, #11531 ) ;
#6189=CARTESIAN_POINT ( 'NONE',  ( -55.33894950108811628, 126.9191314136040063, 167.5679852142817197 ) ) ;
#6190=DIRECTION ( 'NONE',  ( 7.125109674364534776E-05, -0.9999848031710252272, 0.005512562950849704893 ) ) ;
#6215=LINE ( 'NONE', #21810, #9604 ) ;
#6222=CARTESIAN_POINT ( 'NONE',  ( -55.30785090598609344, 143.9326556260107282, 169.9740248546933685 ) ) ;
#6232=VECTOR ( 'NONE', #4118, 1000.000000000000227 ) ;
#6256=ORIENTED_EDGE ( 'NONE', *, *, #14980, .F. ) ;
#6259=VECTOR ( 'NONE', #17992, 999.9999999999998863 ) ;
#6292=AXIS2_PLACEMENT_3D ( 'NONE', #3102, #12069, #1395 ) ;
#6342=DIRECTION ( 'NONE',  ( 0.9999164797902017066, 0.000000000000000000, -0.01292414190463751951 ) ) ;
#6347=CARTESIAN_POINT ( 'NONE',  ( -49.64894119642055870, 126.1473026246197406, 27.48387445644694083 ) ) ;
#6352=ORIENTED_EDGE ( 'NONE', *, *, #4149, .T. ) ;
#6357=VERTEX_POINT ( 'NONE', #18215 ) ;
#6358=AXIS2_PLACEMENT_3D ( 'NONE', #12418, #3556, #5155 ) ;
#6381=ORIENTED_EDGE ( 'NONE', *, *, #13766, .F. ) ;
#6389=AXIS2_PLACEMENT_3D ( 'NONE', #13669, #10642, #15723 ) ;
#6401=EDGE_CURVE ( 'NONE', #11384, #5047, #1087, .T. ) ;
#6445=AXIS2_PLACEMENT_3D ( 'NONE', #1511, #7125, #19405 ) ;
#6454=CARTESIAN_POINT ( 'NONE',  ( -56.08328763590613164, 143.6018742220275044, 109.9799478008652613 ) ) ;
#6455=DIRECTION ( 'NONE',  ( -0.01292394549866738608, -0.005513023399720699824, -0.9999012842304692006 ) ) ;
#6475=CARTESIAN_POINT ( 'NONE',  ( -56.11438623100815448, 126.5883500096207683, 107.5739081604535414 ) ) ;
#6491=EDGE_LOOP ( 'NONE', ( #18356, #14484, #10502 ) ) ;
#6492=ORIENTED_EDGE ( 'NONE', *, *, #9407, .T. ) ;
#6502=DIRECTION ( 'NONE',  ( -0.9999164797902017066, -2.045753974208586179E-15, 0.01292414190464156835 ) ) ;
#6506=ORIENTED_EDGE ( 'NONE', *, *, #7582, .T. ) ;
#6514=EDGE_CURVE ( 'NONE', #12381, #4519, #5301, .T. ) ;
#6535=CIRCLE ( 'NONE', #3214, 3.399999999999986144 ) ;
#6565=CARTESIAN_POINT ( 'NONE',  ( 20.99042507241804145, 140.4227465520236819, 76.49807275461785139 ) ) ;
#6567=EDGE_LOOP ( 'NONE', ( #876, #21816, #10845, #21999 ) ) ;
#6604=CONICAL_SURFACE ( 'NONE', #14336, 2.499999999999988010, 1.029744258676651425 ) ;
#6617=AXIS2_PLACEMENT_3D ( 'NONE', #2228, #3846, #9004 ) ;
#6623=ORIENTED_EDGE ( 'NONE', *, *, #9476, .T. ) ;
#6665=CARTESIAN_POINT ( 'NONE',  ( -18.87699466420334815, 140.4778767860208006, 87.01405127310822252 ) ) ;
#6667=CARTESIAN_POINT ( 'NONE',  ( -44.54898248114630377, 168.6907664596094776, 35.18517999664061335 ) ) ;
#6672=ADVANCED_FACE ( 'NONE', ( #16252 ), #19756, .F. ) ;
#6677=VERTEX_POINT ( 'NONE', #13441 ) ;
#6680=LINE ( 'NONE', #1311, #20591 ) ;
#6755=CARTESIAN_POINT ( 'NONE',  ( 59.65144567478507298, 126.9191314136042479, 166.0817088952479139 ) ) ;
#6772=VERTEX_POINT ( 'NONE', #13662 ) ;
#6786=VECTOR ( 'NONE', #14608, 999.9999999999998863 ) ;
#6794=DIRECTION ( 'NONE',  ( -0.01292394549866738608, -0.005513023399720699824, -0.9999012842304692006 ) ) ;
#6807=CIRCLE ( 'NONE', #3512, 10.00000000000000000 ) ;
#6817=EDGE_CURVE ( 'NONE', #17658, #18467, #4807, .T. ) ;
#6820=DIRECTION ( 'NONE',  ( 7.125109674381880655E-05, -0.9999848031710253382, 0.005512562950849702291 ) ) ;
#6868=DIRECTION ( 'NONE',  ( 7.125109674364534776E-05, -0.9999848031710252272, 0.005512562950849704893 ) ) ;
#6907=VERTEX_POINT ( 'NONE', #7203 ) ;
#6911=CARTESIAN_POINT ( 'NONE',  ( -9.008850598706597879, 165.4223666312992691, 76.74798293798586712 ) ) ;
#6913=AXIS2_PLACEMENT_3D ( 'NONE', #9576, #14772, #16608 ) ;
#6921=ORIENTED_EDGE ( 'NONE', *, *, #14189, .F. ) ;
#6949=CARTESIAN_POINT ( 'NONE',  ( 58.87479767622038906, 143.5880916635284166, 105.9939182712553105 ) ) ;
#6952=VECTOR ( 'NONE', #7739, 999.9999999999998863 ) ;
#6960=DIRECTION ( 'NONE',  ( -0.01292394549866632963, -0.005513023399716958026, -0.9999012842304692006 ) ) ;
#6978=CARTESIAN_POINT ( 'NONE',  ( -45.36474727608069912, 165.8559883853732515, 234.9810740996818197 ) ) ;
#6980=CARTESIAN_POINT ( 'NONE',  ( 58.10057221494500368, 126.2575686056377435, 46.09355478759161429 ) ) ;
#6986=DIRECTION ( 'NONE',  ( 0.8504393858994485633, -0.002839416958724378954, -0.5260653843604455870 ) ) ;
#6987=CARTESIAN_POINT ( 'NONE',  ( 51.42288047930752271, 166.7281037598372961, 233.7252641129099970 ) ) ;
#7023=EDGE_LOOP ( 'NONE', ( #8643, #845, #14519, #16532, #7504, #14191, #901, #10628, #16292, #20234, #7765, #20073 ) ) ;
#7028=ADVANCED_FACE ( 'NONE', ( #14693, #9492, #4204, #8117 ), #13308, .F. ) ;
#7060=FACE_OUTER_BOUND ( 'NONE', #16627, .T. ) ;
#7072=CIRCLE ( 'NONE', #11864, 3.399999999999986144 ) ;
#7088=ORIENTED_EDGE ( 'NONE', *, *, #17310, .T. ) ;
#7101=EDGE_CURVE ( 'NONE', #6357, #12249, #16040, .T. ) ;
#7108=VECTOR ( 'NONE', #22664, 1000.000000000000114 ) ;
#7121=CARTESIAN_POINT ( 'NONE',  ( 65.44129831367571626, 190.1904397277867531, 33.64499135954488196 ) ) ;
#7125=DIRECTION ( 'NONE',  ( 0.01292394549866738608, 0.005513023399720699824, 0.9999012842304692006 ) ) ;
#7146=CARTESIAN_POINT ( 'NONE',  ( -44.54898248114630377, 168.6907664596094776, 35.18517999664061335 ) ) ;
#7189=SURFACE_SIDE_STYLE ('',( #8664 ) ) ;
#7203=CARTESIAN_POINT ( 'NONE',  ( -49.64892827247506091, 126.1473081376431367, 27.48487435773119714 ) ) ;
#7234=ORIENTED_EDGE ( 'NONE', *, *, #10354, .T. ) ;
#7246=ADVANCED_FACE ( 'NONE', ( #2567 ), #18434, .F. ) ;
#7247=EDGE_LOOP ( 'NONE', ( #16904, #945, #8027, #14041 ) ) ;
#7248=CARTESIAN_POINT ( 'NONE',  ( 58.87479767622038906, 143.5880916635284166, 105.9939182712553105 ) ) ;
#7282=( LENGTH_UNIT ( ) NAMED_UNIT ( * ) SI_UNIT ( .MILLI., .METRE. ) );
#7291=ORIENTED_EDGE ( 'NONE', *, *, #18538, .F. ) ;
#7300=CARTESIAN_POINT ( 'NONE',  ( -64.54563767617682402, 145.1911235850903381, 35.57320806407841474 ) ) ;
#7302=LINE ( 'NONE', #16307, #21768 ) ;
#7315=LINE ( 'NONE', #7559, #11002 ) ;
#7321=DIRECTION ( 'NONE',  ( -0.01292394549866738608, -0.005513023399720699824, -0.9999012842304692006 ) ) ;
#7325=DIRECTION ( 'NONE',  ( 0.9999164797902017066, 0.000000000000000000, -0.01292414190463751951 ) ) ;
#7327=ORIENTED_EDGE ( 'NONE', *, *, #21040, .F. ) ;
#7348=CIRCLE ( 'NONE', #13957, 2.499999999999988010 ) ;
#7354=LINE ( 'NONE', #20882, #7468 ) ;
#7403=DIRECTION ( 'NONE',  ( -0.01292394549866632963, -0.005513023399716958026, -0.9999012842304692006 ) ) ;
#7418=FACE_OUTER_BOUND ( 'NONE', #11048, .T. ) ;
#7468=VECTOR ( 'NONE', #10668, 999.9999999999998863 ) ;
#7479=CARTESIAN_POINT ( 'NONE',  ( 68.30941429790007646, 191.4143309225247549, 255.6230893828509352 ) ) ;
#7504=ORIENTED_EDGE ( 'NONE', *, *, #5709, .T. ) ;
#7513=AXIS2_PLACEMENT_3D ( 'NONE', #14795, #15006, #20262 ) ;
#7543=CARTESIAN_POINT ( 'NONE',  ( -47.66114072508762689, 168.8134312302532862, 57.47692565324432934 ) ) ;
#7546=EDGE_CURVE ( 'NONE', #3194, #18220, #478, .T. ) ;
#7559=CARTESIAN_POINT ( 'NONE',  ( -64.54884397553028919, 190.1904397277864973, 35.32514273129018534 ) ) ;
#7582=EDGE_CURVE ( 'NONE', #17225, #11720, #12669, .T. ) ;
#7599=DIRECTION ( 'NONE',  ( -0.01292394549866632963, -0.005513023399716958026, -0.9999012842304692006 ) ) ;
#7607=ORIENTED_EDGE ( 'NONE', *, *, #13993, .F. ) ;
#7627=DIRECTION ( 'NONE',  ( 0.01111468050521610164, -0.5103046645782707280, 0.8599218645824314722 ) ) ;
#7635=AXIS2_PLACEMENT_3D ( 'NONE', #11358, #5834, #11016 ) ;
#7672=PLANE ( 'NONE',  #13584 ) ;
#7684=AXIS2_PLACEMENT_3D ( 'NONE', #7248, #14628, #16019 ) ;
#7686=CARTESIAN_POINT ( 'NONE',  ( -64.64902924016615771, 145.1470193978925636, 27.57399779023469932 ) ) ;
#7692=ADVANCED_FACE ( 'NONE', ( #9418 ), #20087, .T. ) ;
#7705=EDGE_LOOP ( 'NONE', ( #7234, #16577, #7922, #15242 ) ) ;
#7722=ORIENTED_EDGE ( 'NONE', *, *, #1491, .T. ) ;
#7726=CIRCLE ( 'NONE', #763, 3.399999999999992806 ) ;
#7739=DIRECTION ( 'NONE',  ( 7.125109674364536131E-05, -0.9999848031710253382, 0.005512562950849705760 ) ) ;
#7743=CARTESIAN_POINT ( 'NONE',  ( -19.00908416305977156, 180.4221386788646271, 76.79453591276953262 ) ) ;
#7765=ORIENTED_EDGE ( 'NONE', *, *, #1491, .F. ) ;
#7805=DIRECTION ( 'NONE',  ( -0.9999164797902015955, -2.044556590511377167E-15, 0.01292414190464178346 ) ) ;
#7825=DIRECTION ( 'NONE',  ( -0.01292394549866738608, -0.005513023399720698957, -0.9999012842304692006 ) ) ;
#7837=FACE_BOUND ( 'NONE', #4007, .T. ) ;
#7845=AXIS2_PLACEMENT_3D ( 'NONE', #3715, #17984, #12699 ) ;
#7857=CARTESIAN_POINT ( 'NONE',  ( -16.68277397329964273, 181.4144828908143552, 256.7767670742539963 ) ) ;
#7862=AXIS2_PLACEMENT_3D ( 'NONE', #1597, #103, #8586 ) ;
#7867=ORIENTED_EDGE ( 'NONE', *, *, #3164, .F. ) ;
#7883=CARTESIAN_POINT ( 'NONE',  ( -44.26142469380095434, 168.8134312302532862, 57.43298357076854899 ) ) ;
#7890=EDGE_CURVE ( 'NONE', #5077, #16867, #2980, .T. ) ;
#7895=ORIENTED_EDGE ( 'NONE', *, *, #3198, .T. ) ;
#7918=CARTESIAN_POINT ( 'NONE',  ( -61.67516800463454985, 127.4153035195788561, 257.6560318593087686 ) ) ;
#7922=ORIENTED_EDGE ( 'NONE', *, *, #16418, .T. ) ;
#7937=CARTESIAN_POINT ( 'NONE',  ( -56.11559749965279309, 143.5880916635282176, 107.4801945902891021 ) ) ;
#7954=DIRECTION ( 'NONE',  ( -0.9999164797902015955, -2.045733645417851287E-15, 0.01292414190464156835 ) ) ;
#7957=ORIENTED_EDGE ( 'NONE', *, *, #18375, .T. ) ;
#7971=EDGE_CURVE ( 'NONE', #3748, #18558, #1495, .T. ) ;
#7990=ADVANCED_FACE ( 'NONE', ( #1608 ), #2289, .F. ) ;
#8002=CARTESIAN_POINT ( 'NONE',  ( -41.96503124479402658, 165.8559883853732515, 234.9371320172060678 ) ) ;
#8018=ORIENTED_EDGE ( 'NONE', *, *, #21294, .F. ) ;
#8021=CARTESIAN_POINT ( 'NONE',  ( 42.33134245603051937, 168.8134312302534283, 56.31375288182659489 ) ) ;
#8027=ORIENTED_EDGE ( 'NONE', *, *, #15132, .T. ) ;
#8037=CARTESIAN_POINT ( 'NONE',  ( 58.06826235119833512, 126.2437860471384568, 43.59380157701544789 ) ) ;
#8038=ORIENTED_EDGE ( 'NONE', *, *, #7890, .F. ) ;
#8048=CIRCLE ( 'NONE', #18335, 2.499999999999988010 ) ;
#8116=ORIENTED_EDGE ( 'NONE', *, *, #18153, .T. ) ;
#8117=FACE_OUTER_BOUND ( 'NONE', #18940, .T. ) ;
#8123=ORIENTED_EDGE ( 'NONE', *, *, #7101, .F. ) ;
#8125=ADVANCED_FACE ( 'NONE', ( #9283 ), #2304, .F. ) ;
#8133=CARTESIAN_POINT ( 'NONE',  ( 65.33690683320658366, 190.1463355405889786, 25.64579400984300150 ) ) ;
#8148=ADVANCED_FACE ( 'NONE', ( #4556 ), #2843, .F. ) ;
#8154=LINE ( 'NONE', #15183, #18078 ) ;
#8185=DIRECTION ( 'NONE',  ( -0.01292394549866738608, -0.005513023399720698957, -0.9999012842304692006 ) ) ;
#8196=CARTESIAN_POINT ( 'NONE',  ( -46.67741832313596717, 141.4150907639732679, 257.3849938494272465 ) ) ;
#8204=CARTESIAN_POINT ( 'NONE',  ( 58.84369908111836622, 126.5745674511216947, 103.5878786308435906 ) ) ;
#8206=DIRECTION ( 'NONE',  ( 7.125109674364536131E-05, -0.9999848031710253382, 0.005512562950849705760 ) ) ;
#8232=VECTOR ( 'NONE', #919, 1000.000000000000000 ) ;
#8242=EDGE_CURVE ( 'NONE', #4784, #3676, #4103, .T. ) ;
#8290=PLANE ( 'NONE',  #8736 ) ;
#8307=DIRECTION ( 'NONE',  ( 7.125109674364534776E-05, -0.9999848031710252272, 0.005512562950849704893 ) ) ;
#8346=ORIENTED_EDGE ( 'NONE', *, *, #3198, .F. ) ;
#8360=CIRCLE ( 'NONE', #3966, 3.399999999999992806 ) ;
#8409=ORIENTED_EDGE ( 'NONE', *, *, #3491, .F. ) ;
#8444=VECTOR ( 'NONE', #19646, 1000.000000000000227 ) ;
#8486=LINE ( 'NONE', #6665, #1182 ) ;
#8512=AXIS2_PLACEMENT_3D ( 'NONE', #9826, #6820, #4530 ) ;
#8515=CARTESIAN_POINT ( 'NONE',  ( 58.87600894486503478, 126.5883500096209815, 106.0876318414197499 ) ) ;
#8549=CIRCLE ( 'NONE', #6358, 2.499999999999988010 ) ;
#8556=CIRCLE ( 'NONE', #14826, 2.499999999999988010 ) ;
#8586=DIRECTION ( 'NONE',  ( 0.01292394549866738782, 0.005513023399720700692, 0.9999012842304693116 ) ) ;
#8588=CARTESIAN_POINT ( 'NONE',  ( 58.09936094630035797, 143.2573102595451928, 45.99984121742717491 ) ) ;
#8599=DIRECTION ( 'NONE',  ( -0.01292394549866632963, -0.005513023399716958026, -0.9999012842304692006 ) ) ;
#8618=EDGE_LOOP ( 'NONE', ( #9970, #18174, #1866, #22480 ) ) ;
#8627=CARTESIAN_POINT ( 'NONE',  ( -56.85751309718151703, 126.2713511641368171, 50.07958431720155090 ) ) ;
#8643=ORIENTED_EDGE ( 'NONE', *, *, #3168, .T. ) ;
#8648=CARTESIAN_POINT ( 'NONE',  ( -56.11438623100815448, 126.5883500096207683, 107.5739081604535414 ) ) ;
#8664=SURFACE_STYLE_FILL_AREA ( #18002 ) ;
#8677=VERTEX_POINT ( 'NONE', #2833 ) ;
#8695=DIRECTION ( 'NONE',  ( 0.01292394549866738608, 0.005513023399720699824, 0.9999012842304692006 ) ) ;
#8699=CARTESIAN_POINT ( 'NONE',  ( 59.65023440614042727, 143.9188730675116688, 165.9879953250834603 ) ) ;
#8719=ORIENTED_EDGE ( 'NONE', *, *, #14419, .F. ) ;
#8724=FACE_OUTER_BOUND ( 'NONE', #11861, .T. ) ;
#8736=AXIS2_PLACEMENT_3D ( 'NONE', #6565, #18735, #11632 ) ;
#8768=ORIENTED_EDGE ( 'NONE', *, *, #3172, .T. ) ;
#8786=CARTESIAN_POINT ( 'NONE',  ( 20.99042507241804145, 140.4227465520236819, 76.49807275461785139 ) ) ;
#8801=CONICAL_SURFACE ( 'NONE', #6617, 2.499999999999988010, 1.029744258676651425 ) ;
#8808=DIRECTION ( 'NONE',  ( -0.01292394549866632963, -0.005513023399716958026, -0.9999012842304692006 ) ) ;
#8816=CARTESIAN_POINT ( 'NONE',  ( 49.13077451860386446, 168.8134312302534283, 56.22586871687502708 ) ) ;
#8826=VERTEX_POINT ( 'NONE', #22643 ) ;
#8836=CARTESIAN_POINT ( 'NONE',  ( -56.92213282467484703, 126.2437860471382294, 45.08007789604923232 ) ) ;
#8842=VECTOR ( 'NONE', #8871, 999.9999999999998863 ) ;
#8868=LINE ( 'NONE', #19554, #13254 ) ;
#8870=VECTOR ( 'NONE', #14513, 999.9999999999998863 ) ;
#8871=DIRECTION ( 'NONE',  ( -7.125109674364536131E-05, 0.9999848031710253382, -0.005512562950849705760 ) ) ;
#8897=ORIENTED_EDGE ( 'NONE', *, *, #15393, .T. ) ;
#8902=DIRECTION ( 'NONE',  ( -0.01292394549866632963, -0.005513023399716958026, -0.9999012842304692006 ) ) ;
#8948=FACE_BOUND ( 'NONE', #1587, .T. ) ;
#8949=APPLICATION_CONTEXT ( 'automotive_design' ) ;
#8982=DIRECTION ( 'NONE',  ( 7.125109674364534776E-05, -0.9999848031710252272, 0.005512562950849704893 ) ) ;
#8992=EDGE_CURVE ( 'NONE', #17081, #19439, #19351, .T. ) ;
#9004=DIRECTION ( 'NONE',  ( -0.01292394549866632963, -0.005513023399716958026, -0.9999012842304692006 ) ) ;
#9005=SHAPE_REPRESENTATION_RELATIONSHIP ( 'NONE' , 'NONE' ,  #10182, #16783 ) ;
#9008=EDGE_LOOP ( 'NONE', ( #20921, #10690 ) ) ;
#9041=DIRECTION ( 'NONE',  ( -0.01292394549866632963, -0.005513023399716958026, -0.9999012842304692006 ) ) ;
#9048=CARTESIAN_POINT ( 'NONE',  ( 51.71043826665287924, 166.8507685304810764, 255.9730676870379114 ) ) ;
#9049=ADVANCED_FACE ( 'NONE', ( #4061 ), #20125, .F. ) ;
#9052=CONICAL_SURFACE ( 'NONE', #17903, 2.499999999999988010, 1.029744258676651425 ) ;
#9124=CIRCLE ( 'NONE', #20134, 2.499999999999988010 ) ;
#9131=VERTEX_POINT ( 'NONE', #6026 ) ;
#9141=DIRECTION ( 'NONE',  ( -0.01104128644981183967, -0.5197558313507629757, -0.8542435049623791077 ) ) ;
#9153=AXIS2_PLACEMENT_3D ( 'NONE', #18636, #2797, #2897 ) ;
#9176=CIRCLE ( 'NONE', #3302, 2.499999999999988010 ) ;
#9182=ORIENTED_EDGE ( 'NONE', *, *, #10898, .T. ) ;
#9234=VECTOR ( 'NONE', #19742, 999.9999999999998863 ) ;
#9238=ORIENTED_EDGE ( 'NONE', *, *, #2654, .F. ) ;
#9241=ORIENTED_EDGE ( 'NONE', *, *, #2649, .T. ) ;
#9249=CARTESIAN_POINT ( 'NONE',  ( 68.30941429790007646, 191.4143309225247549, 255.6230893828509352 ) ) ;
#9264=ORIENTED_EDGE ( 'NONE', *, *, #743, .T. ) ;
#9272=ORIENTED_EDGE ( 'NONE', *, *, #18910, .F. ) ;
#9283=FACE_OUTER_BOUND ( 'NONE', #19137, .T. ) ;
#9284=CONICAL_SURFACE ( 'NONE', #18476, 3.399999999999986144, 1.029744258676653201 ) ;
#9305=VECTOR ( 'NONE', #14541, 1000.000000000000227 ) ;
#9315=LINE ( 'NONE', #16360, #16773 ) ;
#9317=ORIENTED_EDGE ( 'NONE', *, *, #12019, .T. ) ;
#9327=CARTESIAN_POINT ( 'NONE',  ( 58.13288207869166513, 126.2713511641370445, 48.59330799816777358 ) ) ;
#9342=FACE_OUTER_BOUND ( 'NONE', #18653, .T. ) ;
#9348=CARTESIAN_POINT ( 'NONE',  ( -38.56531521350737535, 165.8559883853732515, 234.8931899347302874 ) ) ;
#9360=EDGE_CURVE ( 'NONE', #19120, #1243, #89, .T. ) ;
#9366=AXIS2_PLACEMENT_3D ( 'NONE', #6189, #20186, #13442 ) ;
#9395=LINE ( 'NONE', #796, #12385 ) ;
#9407=EDGE_CURVE ( 'NONE', #17658, #10714, #10155, .T. ) ;
#9418=FACE_OUTER_BOUND ( 'NONE', #7705, .T. ) ;
#9460=( GEOMETRIC_REPRESENTATION_CONTEXT ( 3 ) GLOBAL_UNCERTAINTY_ASSIGNED_CONTEXT ( ( #1881 ) ) GLOBAL_UNIT_ASSIGNED_CONTEXT ( ( #12716, #12261, #3952 ) ) REPRESENTATION_CONTEXT ( 'NONE', 'WORKASPACE' ) );
#9466=EDGE_CURVE ( 'NONE', #11266, #10714, #13980, .T. ) ;
#9472=FACE_OUTER_BOUND ( 'NONE', #19832, .T. ) ;
#9476=EDGE_CURVE ( 'NONE', #3676, #9640, #16930, .T. ) ;
#9481=CARTESIAN_POINT ( 'NONE',  ( 65.34146690339817098, 126.1473081376433498, 25.99859803869739139 ) ) ;
#9490=ORIENTED_EDGE ( 'NONE', *, *, #2105, .F. ) ;
#9491=CIRCLE ( 'NONE', #6178, 10.00000000000000711 ) ;
#9492=FACE_BOUND ( 'NONE', #22400, .T. ) ;
#9507=ADVANCED_FACE ( 'NONE', ( #4849 ), #11993, .F. ) ;
#9509=VECTOR ( 'NONE', #21792, 999.9999999999998863 ) ;
#9514=EDGE_CURVE ( 'NONE', #12249, #11335, #1758, .T. ) ;
#9520=CARTESIAN_POINT ( 'NONE',  ( -61.67972807482614428, 191.4143309225244707, 257.3032278304543183 ) ) ;
#9530=DIRECTION ( 'NONE',  ( -0.01292394549866632963, -0.005513023399716958026, -0.9999012842304692006 ) ) ;
#9564=VERTEX_POINT ( 'NONE', #3237 ) ;
#9570=ORIENTED_EDGE ( 'NONE', *, *, #14157, .F. ) ;
#9576=CARTESIAN_POINT ( 'NONE',  ( 58.10057221494500368, 126.2575686056377435, 46.09355478759161429 ) ) ;
#9592=VECTOR ( 'NONE', #8206, 999.9999999999998863 ) ;
#9604=VECTOR ( 'NONE', #14969, 1000.000000000000114 ) ;
#9634=CONICAL_SURFACE ( 'NONE', #22437, 2.499999999999988010, 1.029744258676651425 ) ;
#9640=VERTEX_POINT ( 'NONE', #5528 ) ;
#9649=DIRECTION ( 'NONE',  ( 0.8637520339192008567, 0.002839416958727990648, 0.5039090806998601790 ) ) ;
#9654=ORIENTED_EDGE ( 'NONE', *, *, #18538, .T. ) ;
#9716=CARTESIAN_POINT ( 'NONE',  ( 65.44450461302918143, 145.1911235850906223, 33.89305669233311136 ) ) ;
#9723=AXIS2_PLACEMENT_3D ( 'NONE', #1237, #11793, #3049 ) ;
#9725=ORIENTED_EDGE ( 'NONE', *, *, #20428, .T. ) ;
#9775=DIRECTION ( 'NONE',  ( -7.125109674364536131E-05, 0.9999848031710253382, -0.005512562950849706628 ) ) ;
#9790=ORIENTED_EDGE ( 'NONE', *, *, #666, .T. ) ;
#9791=CARTESIAN_POINT ( 'NONE',  ( 47.99676178238597402, 166.7168410604182327, 231.7264817597146020 ) ) ;
#9803=LINE ( 'NONE', #16818, #11692 ) ;
#9804=PLANE ( 'NONE',  #18794 ) ;
#9819=FACE_OUTER_BOUND ( 'NONE', #14643, .T. ) ;
#9826=CARTESIAN_POINT ( 'NONE',  ( -8.880679910171080493, 180.4772689128618595, 86.66430733602781800 ) ) ;
#9860=DIRECTION ( 'NONE',  ( 7.125109674364534776E-05, -0.9999848031710252272, 0.005512562950849704026 ) ) ;
#9868=CONICAL_SURFACE ( 'NONE', #21219, 3.399999999999986144, 1.029744258676653201 ) ;
#9874=ORIENTED_EDGE ( 'NONE', *, *, #2654, .T. ) ;
#9885=ORIENTED_EDGE ( 'NONE', *, *, #7890, .T. ) ;
#9904=VECTOR ( 'NONE', #18916, 1000.000000000000227 ) ;
#9907=ADVANCED_FACE ( 'NONE', ( #12419 ), #20729, .F. ) ;
#9915=ORIENTED_EDGE ( 'NONE', *, *, #12819, .T. ) ;
#9933=ADVANCED_FACE ( 'NONE', ( #21020 ), #20786, .F. ) ;
#9935=ADVANCED_FACE ( 'NONE', ( #15425 ), #15649, .F. ) ;
#9943=CYLINDRICAL_SURFACE ( 'NONE', #3644, 3.399999999999986144 ) ;
#9950=EDGE_LOOP ( 'NONE', ( #14096, #14209, #15213 ) ) ;
#9970=ORIENTED_EDGE ( 'NONE', *, *, #9514, .F. ) ;
#9975=CARTESIAN_POINT ( 'NONE',  ( -16.68277397329964273, 181.4144828908143552, 256.7767670742539963 ) ) ;
#9988=VECTOR ( 'NONE', #13860, 999.9999999999998863 ) ;
#10038=LINE ( 'NONE', #6911, #3929 ) ;
#10044=AXIS2_PLACEMENT_3D ( 'NONE', #512, #12927, #4383 ) ;
#10054=VECTOR ( 'NONE', #19284, 999.9999999999998863 ) ;
#10056=ORIENTED_EDGE ( 'NONE', *, *, #4162, .T. ) ;
#10073=DIRECTION ( 'NONE',  ( 0.9999164797902015955, 0.000000000000000000, -0.01292414190463754553 ) ) ;
#10075=EDGE_CURVE ( 'NONE', #4519, #11414, #11021, .T. ) ;
#10102=DIRECTION ( 'NONE',  ( 0.01292394549866738608, 0.005513023399720699824, 0.9999012842304692006 ) ) ;
#10118=ORIENTED_EDGE ( 'NONE', *, *, #12019, .F. ) ;
#10128=EDGE_CURVE ( 'NONE', #15200, #5640, #10475, .T. ) ;
#10147=ORIENTED_EDGE ( 'NONE', *, *, #4777, .F. ) ;
#10149=DIRECTION ( 'NONE',  ( 7.125109674364534776E-05, -0.9999848031710252272, 0.005512562950849704893 ) ) ;
#10155=LINE ( 'NONE', #22411, #9592 ) ;
#10168=FACE_OUTER_BOUND ( 'NONE', #3869, .T. ) ;
#10169=FACE_OUTER_BOUND ( 'NONE', #22110, .T. ) ;
#10173=FACE_OUTER_BOUND ( 'NONE', #1633, .T. ) ;
#10182=SHAPE_REPRESENTATION ( 'Moving Jaw', ( #6292 ), #11807 ) ;
#10185=EDGE_CURVE ( 'NONE', #20596, #11089, #15176, .T. ) ;
#10201=EDGE_CURVE ( 'NONE', #5047, #4519, #19964, .T. ) ;
#10214=CONICAL_SURFACE ( 'NONE', #4324, 3.399999999999986144, 1.029744258676653201 ) ;
#10215=ORIENTED_EDGE ( 'NONE', *, *, #18229, .T. ) ;
#10221=CARTESIAN_POINT ( 'NONE',  ( 48.02316444802085016, 166.7281037598372961, 233.7692061953857774 ) ) ;
#10222=EDGE_LOOP ( 'NONE', ( #5045, #4195, #14570, #7895 ) ) ;
#10231=CARTESIAN_POINT ( 'NONE',  ( 10.98947899709743581, 165.4223666312993259, 76.48950009989302146 ) ) ;
#10251=FACE_OUTER_BOUND ( 'NONE', #10222, .T. ) ;
#10256=CARTESIAN_POINT ( 'NONE',  ( 48.31072223536619958, 166.8507685304810764, 256.0170097695137201 ) ) ;
#10281=DIRECTION ( 'NONE',  ( -0.01292394549866632963, -0.005513023399716958026, -0.9999012842304692006 ) ) ;
#10297=AXIS2_PLACEMENT_3D ( 'NONE', #14634, #2851, #7599 ) ;
#10299=EDGE_CURVE ( 'NONE', #13257, #165, #6807, .T. ) ;
#10302=CONICAL_SURFACE ( 'NONE', #2920, 2.499999999999988010, 1.029744258676651425 ) ;
#10313=VERTEX_POINT ( 'NONE', #14402 ) ;
#10326=PLANE ( 'NONE',  #7862 ) ;
#10334=VECTOR ( 'NONE', #17162, 999.9999999999998863 ) ;
#10343=DIRECTION ( 'NONE',  ( 7.125109674364534776E-05, -0.9999848031710252272, 0.005512562950849704893 ) ) ;
#10350=FACE_OUTER_BOUND ( 'NONE', #19770, .T. ) ;
#10354=EDGE_CURVE ( 'NONE', #17225, #4965, #5739, .T. ) ;
#10371=CIRCLE ( 'NONE', #8512, 10.00000000000000000 ) ;
#10376=EDGE_LOOP ( 'NONE', ( #17336, #757, #12843, #18455 ) ) ;
#10394=LINE ( 'NONE', #5203, #3971 ) ;
#10403=AXIS2_PLACEMENT_3D ( 'NONE', #20240, #4503, #20696 ) ;
#10417=ORIENTED_EDGE ( 'NONE', *, *, #20310, .F. ) ;
#10425=CARTESIAN_POINT ( 'NONE',  ( 58.09936094630035797, 143.2573102595451928, 45.99984121742717491 ) ) ;
#10447=CARTESIAN_POINT ( 'NONE',  ( 21.11966452740471567, 140.4778767860209143, 86.49708559692257381 ) ) ;
#10475=CIRCLE ( 'NONE', #9366, 2.499999999999988010 ) ;
#10502=ORIENTED_EDGE ( 'NONE', *, *, #656, .T. ) ;
#10526=CARTESIAN_POINT ( 'NONE',  ( 10.99126027451603171, 140.4227465520236535, 76.62731417366427422 ) ) ;
#10548=DIRECTION ( 'NONE',  ( -0.01292394549866632963, -0.005513023399716958026, -0.9999012842304692006 ) ) ;
#10563=CARTESIAN_POINT ( 'NONE',  ( -56.11438623100815448, 126.5883500096207683, 107.5739081604535414 ) ) ;
#10584=CARTESIAN_POINT ( 'NONE',  ( -55.33894950108811628, 126.9191314136040063, 167.5679852142817197 ) ) ;
#10588=CARTESIAN_POINT ( 'NONE',  ( 65.34111304903984774, 145.1470193978928478, 25.89384641848939239 ) ) ;
#10625=EDGE_LOOP ( 'NONE', ( #21570, #22473, #8897 ) ) ;
#10628=ORIENTED_EDGE ( 'NONE', *, *, #8992, .F. ) ;
#10634=EDGE_LOOP ( 'NONE', ( #7291, #15880, #20127, #8 ) ) ;
#10638=ADVANCED_FACE ( 'NONE', ( #22359 ), #10867, .F. ) ;
#10642=DIRECTION ( 'NONE',  ( 7.125109674364534776E-05, -0.9999848031710252272, 0.005512562950849704893 ) ) ;
#10649=ORIENTED_EDGE ( 'NONE', *, *, #22012, .F. ) ;
#10656=ORIENTED_EDGE ( 'NONE', *, *, #10354, .F. ) ;
#10668=DIRECTION ( 'NONE',  ( 7.125109674364536131E-05, -0.9999848031710253382, 0.005512562950849705760 ) ) ;
#10690=ORIENTED_EDGE ( 'NONE', *, *, #17310, .F. ) ;
#10691=CARTESIAN_POINT ( 'NONE',  ( 50.34170926724522843, 140.1470898690143372, 26.11428438467088142 ) ) ;
#10699=AXIS2_PLACEMENT_3D ( 'NONE', #4782, #5121, #13992 ) ;
#10714=VERTEX_POINT ( 'NONE', #15524 ) ;
#10720=ORIENTED_EDGE ( 'NONE', *, *, #19390, .F. ) ;
#10745=CARTESIAN_POINT ( 'NONE',  ( 58.87600894486503478, 126.5883500096209815, 106.0876318414197499 ) ) ;
#10760=CARTESIAN_POINT ( 'NONE',  ( -64.54884397553028919, 190.1904397277864973, 35.32514273129017113 ) ) ;
#10783=EDGE_CURVE ( 'NONE', #5077, #11631, #12239, .T. ) ;
#10790=CIRCLE ( 'NONE', #21758, 2.499999999999988010 ) ;
#10793=LINE ( 'NONE', #8816, #13974 ) ;
#10800=CIRCLE ( 'NONE', #21066, 3.399999999999986144 ) ;
#10823=ORIENTED_EDGE ( 'NONE', *, *, #17599, .F. ) ;
#10834=CARTESIAN_POINT ( 'NONE',  ( 53.31522717123864652, 127.4153035195790835, 256.1697555402749913 ) ) ;
#10841=ORIENTED_EDGE ( 'NONE', *, *, #17934, .F. ) ;
#10842=LINE ( 'NONE', #17621, #8842 ) ;
#10845=ORIENTED_EDGE ( 'NONE', *, *, #11289, .T. ) ;
#10867=CONICAL_SURFACE ( 'NONE', #14934, 2.499999999999988010, 1.029744258676651425 ) ;
#10872=CARTESIAN_POINT ( 'NONE',  ( -41.96503124479402658, 165.8559883853732515, 234.9371320172060678 ) ) ;
#10891=ADVANCED_FACE ( 'NONE', ( #17179 ), #11792, .F. ) ;
#10896=FACE_OUTER_BOUND ( 'NONE', #18192, .T. ) ;
#10898=EDGE_CURVE ( 'NONE', #16237, #12381, #11673, .T. ) ;
#10909=PLANE ( 'NONE',  #7635 ) ;
#10955=FACE_OUTER_BOUND ( 'NONE', #22069, .T. ) ;
#10956=ADVANCED_FACE ( 'NONE', ( #10168 ), #9284, .F. ) ;
#10972=EDGE_CURVE ( 'NONE', #530, #21215, #8556, .T. ) ;
#10976=CARTESIAN_POINT ( 'NONE',  ( 45.73105848731719192, 168.8134312302534283, 56.26981079935081453 ) ) ;
#10988=DIRECTION ( 'NONE',  ( -0.01292394549866738608, -0.005513023399720699824, -0.9999012842304692006 ) ) ;
#11002=VECTOR ( 'NONE', #19605, 1000.000000000000114 ) ;
#11010=ADVANCED_FACE ( 'NONE', ( #15932 ), #19112, .F. ) ;
#11016=DIRECTION ( 'NONE',  ( -0.9999164797902015955, -2.219203356785934189E-15, 0.01292414190464157009 ) ) ;
#11021=LINE ( 'NONE', #19727, #6786 ) ;
#11048=EDGE_LOOP ( 'NONE', ( #10823, #10656, #6506, #3693, #14728, #635 ) ) ;
#11074=VECTOR ( 'NONE', #17589, 999.9999999999998863 ) ;
#11079=LINE ( 'NONE', #12702, #1249 ) ;
#11087=DIRECTION ( 'NONE',  ( -7.125109674381880655E-05, 0.9999848031710252272, -0.005512562950849702291 ) ) ;
#11089=VERTEX_POINT ( 'NONE', #9348 ) ;
#11120=ORIENTED_EDGE ( 'NONE', *, *, #20722, .F. ) ;
#11126=DIRECTION ( 'NONE',  ( -0.01292394549866632963, -0.005513023399716958026, -0.9999012842304692006 ) ) ;
#11136=DIRECTION ( 'NONE',  ( -0.9999164797902015955, 0.000000000000000000, 0.01292414190464162733 ) ) ;
#11143=LINE ( 'NONE', #19962, #5931 ) ;
#11148=DIRECTION ( 'NONE',  ( -0.01292394549866632963, -0.005513023399716958026, -0.9999012842304692006 ) ) ;
#11174=EDGE_CURVE ( 'NONE', #3247, #1930, #11079, .T. ) ;
#11212=EDGE_CURVE ( 'NONE', #8826, #12249, #3452, .T. ) ;
#11233=VERTEX_POINT ( 'NONE', #13493 ) ;
#11238=VECTOR ( 'NONE', #7825, 1000.000000000000114 ) ;
#11266=VERTEX_POINT ( 'NONE', #4624 ) ;
#11286=ORIENTED_EDGE ( 'NONE', *, *, #91, .F. ) ;
#11289=EDGE_CURVE ( 'NONE', #9564, #9131, #1986, .T. ) ;
#11335=VERTEX_POINT ( 'NONE', #8627 ) ;
#11358=CARTESIAN_POINT ( 'NONE',  ( -19.00908416305977156, 180.4221386788646271, 76.79453591276953262 ) ) ;
#11384=VERTEX_POINT ( 'NONE', #22614 ) ;
#11398=ORIENTED_EDGE ( 'NONE', *, *, #13633, .T. ) ;
#11414=VERTEX_POINT ( 'NONE', #10834 ) ;
#11428=ORIENTED_EDGE ( 'NONE', *, *, #11943, .T. ) ;
#11433=LINE ( 'NONE', #11552, #20345 ) ;
#11447=EDGE_CURVE ( 'NONE', #2088, #11384, #3577, .T. ) ;
#11464=ADVANCED_FACE ( 'NONE', ( #14059 ), #5401, .F. ) ;
#11475=ORIENTED_EDGE ( 'NONE', *, *, #21450, .F. ) ;
#11495=ORIENTED_EDGE ( 'NONE', *, *, #3822, .T. ) ;
#11517=VECTOR ( 'NONE', #5025, 999.9999999999998863 ) ;
#11531=DIRECTION ( 'NONE',  ( 0.01292394549866729934, 0.005513023399719703226, 0.9999012842304692006 ) ) ;
#11543=CIRCLE ( 'NONE', #13011, 2.499999999999988010 ) ;
#11552=CARTESIAN_POINT ( 'NONE',  ( 65.44129831367571626, 190.1904397277867531, 33.64499135954488196 ) ) ;
#11562=CYLINDRICAL_SURFACE ( 'NONE', #2564, 2.499999999999988010 ) ;
#11590=CARTESIAN_POINT ( 'NONE',  ( -55.30663963734144772, 126.9329139721032931, 170.0677384248578790 ) ) ;
#11594=CARTESIAN_POINT ( 'NONE',  ( 59.61792454239376582, 143.9050905090123820, 163.4882421145072726 ) ) ;
#11617=ORIENTED_EDGE ( 'NONE', *, *, #1716, .F. ) ;
#11631=VERTEX_POINT ( 'NONE', #22260 ) ;
#11632=DIRECTION ( 'NONE',  ( -7.125109674381882011E-05, 0.9999848031710253382, -0.005512562950849702291 ) ) ;
#11647=DIRECTION ( 'NONE',  ( 7.125109674364534776E-05, -0.9999848031710252272, 0.005512562950849704893 ) ) ;
#11673=LINE ( 'NONE', #5087, #17764 ) ;
#11692=VECTOR ( 'NONE', #1072, 1000.000000000000227 ) ;
#11720=VERTEX_POINT ( 'NONE', #22158 ) ;
#11727=LINE ( 'NONE', #10231, #12487 ) ;
#11731=CARTESIAN_POINT ( 'NONE',  ( -18.87984470807310089, 180.4772689128618310, 86.79354875507422662 ) ) ;
#11734=EDGE_CURVE ( 'NONE', #22035, #17658, #1396, .T. ) ;
#11748=DIRECTION ( 'NONE',  ( 7.125109674364534776E-05, -0.9999848031710252272, 0.005512562950849704893 ) ) ;
#11779=EDGE_LOOP ( 'NONE', ( #14099, #3004, #15909 ) ) ;
#11792=PLANE ( 'NONE',  #21743 ) ;
#11793=DIRECTION ( 'NONE',  ( 0.01292394549866738608, 0.005513023399720699824, 0.9999012842304692006 ) ) ;
#11807=( GEOMETRIC_REPRESENTATION_CONTEXT ( 3 ) GLOBAL_UNCERTAINTY_ASSIGNED_CONTEXT ( ( #1666 ) ) GLOBAL_UNIT_ASSIGNED_CONTEXT ( ( #7282, #3392, #287 ) ) REPRESENTATION_CONTEXT ( 'NONE', 'WORKASPACE' ) );
#11811=AXIS2_PLACEMENT_3D ( 'NONE', #900, #4426, #16856 ) ;
#11841=DIRECTION ( 'NONE',  ( 7.125109674381882011E-05, -0.9999848031710253382, 0.005512562950849702291 ) ) ;
#11848=ORIENTED_EDGE ( 'NONE', *, *, #3979, .T. ) ;
#11861=EDGE_LOOP ( 'NONE', ( #13098, #18072, #3995 ) ) ;
#11864=AXIS2_PLACEMENT_3D ( 'NONE', #10872, #19360, #21197 ) ;
#11883=CARTESIAN_POINT ( 'NONE',  ( -55.34016076973275489, 143.9188730675114414, 167.4742716441172377 ) ) ;
#11908=DIRECTION ( 'NONE',  ( -0.01292394549866738608, -0.005513023399720699824, -0.9999012842304692006 ) ) ;
#11943=EDGE_CURVE ( 'NONE', #6907, #18256, #2292, .T. ) ;
#11949=CARTESIAN_POINT ( 'NONE',  ( -55.30663963734144772, 126.9329139721032931, 170.0677384248578790 ) ) ;
#11953=DIRECTION ( 'NONE',  ( 0.8637520339192008567, 0.002839416958727990648, 0.5039090806998601790 ) ) ;
#11963=CARTESIAN_POINT ( 'NONE',  ( 59.65144567478507298, 126.9191314136042479, 166.0817088952479139 ) ) ;
#11966=DIRECTION ( 'NONE',  ( 0.01292394549866738782, 0.005513023399720700692, 0.9999012842304693116 ) ) ;
#11973=EDGE_LOOP ( 'NONE', ( #1582, #15050, #4416, #19844, #21715, #15721, #16988, #13812 ) ) ;
#11991=DIRECTION ( 'NONE',  ( 7.125109674364536131E-05, -0.9999848031710253382, 0.005512562950849705760 ) ) ;
#11993=CYLINDRICAL_SURFACE ( 'NONE', #925, 2.499999999999988010 ) ;
#12019=EDGE_CURVE ( 'NONE', #11631, #1653, #6073, .T. ) ;
#12043=APPLICATION_CONTEXT ( 'automotive_design' ) ;
#12045=EDGE_CURVE ( 'NONE', #16756, #3247, #16774, .T. ) ;
#12054=VERTEX_POINT ( 'NONE', #4778 ) ;
#12063=DIRECTION ( 'NONE',  ( 7.125109674364534776E-05, -0.9999848031710252272, 0.005512562950849704893 ) ) ;
#12069=DIRECTION ( 'NONE',  ( 0.000000000000000000, 0.000000000000000000, 1.000000000000000000 ) ) ;
#12075=CARTESIAN_POINT ( 'NONE',  ( -8.879611143719925437, 165.4774968652964731, 86.74699578029056113 ) ) ;
#12089=ORIENTED_EDGE ( 'NONE', *, *, #13782, .F. ) ;
#12112=CONICAL_SURFACE ( 'NONE', #20875, 3.399999999999986144, 1.029744258676653201 ) ;
#12169=DIRECTION ( 'NONE',  ( 0.01292394549866738608, 0.005513023399720699824, 0.9999012842304692006 ) ) ;
#12182=ORIENTED_EDGE ( 'NONE', *, *, #17200, .F. ) ;
#12194=ORIENTED_EDGE ( 'NONE', *, *, #6115, .T. ) ;
#12229=ORIENTED_EDGE ( 'NONE', *, *, #4444, .T. ) ;
#12239=CIRCLE ( 'NONE', #16313, 3.399999999999986144 ) ;
#12249=VERTEX_POINT ( 'NONE', #12276 ) ;
#12261=( NAMED_UNIT ( * ) PLANE_ANGLE_UNIT ( ) SI_UNIT ( $, .RADIAN. ) );
#12272=DIRECTION ( 'NONE',  ( 7.125109674364534776E-05, -0.9999848031710252272, 0.005512562950849704893 ) ) ;
#12276=CARTESIAN_POINT ( 'NONE',  ( -56.85872436582616274, 143.2710928180442522, 49.98587074703709732 ) ) ;
#12277=DIRECTION ( 'NONE',  ( -0.9999164797902015955, 0.000000000000000000, 0.01292414190464162733 ) ) ;
#12305=DIRECTION ( 'NONE',  ( 7.125109674364534776E-05, -0.9999848031710252272, 0.005512562950849704893 ) ) ;
#12343=DIRECTION ( 'NONE',  ( 7.125109674364536131E-05, -0.9999848031710253382, 0.005512562950849705760 ) ) ;
#12376=AXIS2_PLACEMENT_3D ( 'NONE', #18508, #16792, #18605 ) ;
#12377=DIRECTION ( 'NONE',  ( -0.01292394549866632963, -0.005513023399716958026, -0.9999012842304692006 ) ) ;
#12381=VERTEX_POINT ( 'NONE', #18336 ) ;
#12385=VECTOR ( 'NONE', #3985, 1000.000000000000114 ) ;
#12388=ORIENTED_EDGE ( 'NONE', *, *, #676, .F. ) ;
#12418=CARTESIAN_POINT ( 'NONE',  ( 58.10057221494500368, 126.2575686056377435, 46.09355478759161429 ) ) ;
#12419=FACE_OUTER_BOUND ( 'NONE', #14596, .T. ) ;
#12425=EDGE_LOOP ( 'NONE', ( #8123, #21330, #2987 ) ) ;
#12434=ORIENTED_EDGE ( 'NONE', *, *, #14980, .T. ) ;
#12472=DIRECTION ( 'NONE',  ( 7.125109674364534776E-05, -0.9999848031710252272, 0.005512562950849704893 ) ) ;
#12476=CARTESIAN_POINT ( 'NONE',  ( 59.61913581103840443, 126.9053488551049611, 163.5819556846717546 ) ) ;
#12487=VECTOR ( 'NONE', #15204, 999.9999999999998863 ) ;
#12527=CARTESIAN_POINT ( 'NONE',  ( -49.64894119642055870, 126.1473026246197406, 27.48387445644694083 ) ) ;
#12530=CARTESIAN_POINT ( 'NONE',  ( -64.64767546932803555, 126.1473081376431082, 27.67873648630081362 ) ) ;
#12601=EDGE_LOOP ( 'NONE', ( #11617, #4924, #8409, #14406, #22521, #9874 ) ) ;
#12614=ADVANCED_FACE ( 'NONE', ( #5871, #7837, #12904 ), #21708, .F. ) ;
#12654=ORIENTED_EDGE ( 'NONE', *, *, #15558, .F. ) ;
#12669=LINE ( 'NONE', #7479, #8870 ) ;
#12670=VERTEX_POINT ( 'NONE', #9327 ) ;
#12682=ADVANCED_FACE ( 'NONE', ( #15535, #4815, #15206, #17133 ), #3108, .F. ) ;
#12699=DIRECTION ( 'NONE',  ( 0.9999164797902015955, 0.000000000000000000, -0.01292414190463754553 ) ) ;
#12702=CARTESIAN_POINT ( 'NONE',  ( 42.04378466868516995, 168.6907664596096765, 34.06594930769865925 ) ) ;
#12707=ORIENTED_EDGE ( 'NONE', *, *, #10299, .T. ) ;
#12716=( LENGTH_UNIT ( ) NAMED_UNIT ( * ) SI_UNIT ( .MILLI., .METRE. ) );
#12722=VERTEX_POINT ( 'NONE', #11731 ) ;
#12732=ADVANCED_FACE ( 'NONE', ( #15084 ), #4599, .F. ) ;
#12751=VERTEX_POINT ( 'NONE', #4696 ) ;
#12774=CARTESIAN_POINT ( 'NONE',  ( -47.66114072508762689, 168.8134312302532862, 57.47692565324432934 ) ) ;
#12786=ORIENTED_EDGE ( 'NONE', *, *, #20003, .T. ) ;
#12793=EDGE_LOOP ( 'NONE', ( #10147, #1003, #12809, #5823 ) ) ;
#12809=ORIENTED_EDGE ( 'NONE', *, *, #13993, .T. ) ;
#12812=VERTEX_POINT ( 'NONE', #8836 ) ;
#12819=EDGE_CURVE ( 'NONE', #12670, #20506, #8549, .T. ) ;
#12837=DIRECTION ( 'NONE',  ( 7.125109674364534776E-05, -0.9999848031710252272, 0.005512562950849704893 ) ) ;
#12843=ORIENTED_EDGE ( 'NONE', *, *, #22012, .T. ) ;
#12870=LINE ( 'NONE', #19728, #6232 ) ;
#12904=FACE_BOUND ( 'NONE', #15347, .T. ) ;
#12927=DIRECTION ( 'NONE',  ( 7.125109674364534776E-05, -0.9999848031710252272, 0.005512562950849704893 ) ) ;
#12987=ORIENTED_EDGE ( 'NONE', *, *, #14860, .F. ) ;
#13011=AXIS2_PLACEMENT_3D ( 'NONE', #6755, #19150, #8808 ) ;
#13047=ADVANCED_FACE ( 'NONE', ( #17098 ), #20634, .F. ) ;
#13052=ORIENTED_EDGE ( 'NONE', *, *, #2384, .F. ) ;
#13098=ORIENTED_EDGE ( 'NONE', *, *, #1377, .F. ) ;
#13106=DIRECTION ( 'NONE',  ( -0.01292394549866632963, -0.005513023399716958026, -0.9999012842304692006 ) ) ;
#13111=EDGE_LOOP ( 'NONE', ( #13502, #4018 ) ) ;
#13143=AXIS2_PLACEMENT_3D ( 'NONE', #196, #16302, #19251 ) ;
#13147=FACE_OUTER_BOUND ( 'NONE', #8618, .T. ) ;
#13159=ORIENTED_EDGE ( 'NONE', *, *, #14588, .F. ) ;
#13162=DIRECTION ( 'NONE',  ( 0.01292394549866738782, 0.005513023399720700692, 0.9999012842304693116 ) ) ;
#13170=VERTEX_POINT ( 'NONE', #10760 ) ;
#13221=LINE ( 'NONE', #17116, #16138 ) ;
#13254=VECTOR ( 'NONE', #17508, 1000.000000000000227 ) ;
#13257=VERTEX_POINT ( 'NONE', #18450 ) ;
#13284=DIRECTION ( 'NONE',  ( -0.9999164797902015955, -2.045733645417851681E-15, 0.01292414190464156835 ) ) ;
#13308=PLANE ( 'NONE',  #11811 ) ;
#13325=ORIENTED_EDGE ( 'NONE', *, *, #5269, .F. ) ;
#13340=ORIENTED_EDGE ( 'NONE', *, *, #15289, .F. ) ;
#13350=VECTOR ( 'NONE', #17547, 999.9999999999998863 ) ;
#13354=LINE ( 'NONE', #8786, #7108 ) ;
#13373=AXIS2_PLACEMENT_3D ( 'NONE', #19274, #7321, #108 ) ;
#13402=EDGE_LOOP ( 'NONE', ( #10118, #19216, #9885, #21589 ) ) ;
#13424=ORIENTED_EDGE ( 'NONE', *, *, #11289, .F. ) ;
#13441=CARTESIAN_POINT ( 'NONE',  ( 59.68254426988709582, 143.9326556260109555, 168.4877485356595912 ) ) ;
#13442=DIRECTION ( 'NONE',  ( -0.01292394549866632963, -0.005513023399716958026, -0.9999012842304692006 ) ) ;
#13446=ADVANCED_FACE ( 'NONE', ( #19107 ), #21067, .F. ) ;
#13448=LINE ( 'NONE', #7918, #9509 ) ;
#13476=LINE ( 'NONE', #1063, #3617 ) ;
#13478=ADVANCED_FACE ( 'NONE', ( #13147 ), #16487, .F. ) ;
#13483=EDGE_LOOP ( 'NONE', ( #7867, #12707, #20123, #621, #7327, #9654 ) ) ;
#13484=LINE ( 'NONE', #18005, #841 ) ;
#13493=CARTESIAN_POINT ( 'NONE',  ( 44.62344841673415630, 166.7281037598372961, 233.8131482778615577 ) ) ;
#13502=ORIENTED_EDGE ( 'NONE', *, *, #9466, .F. ) ;
#13563=ORIENTED_EDGE ( 'NONE', *, *, #10185, .F. ) ;
#13570=DIRECTION ( 'NONE',  ( -7.125109674364536131E-05, 0.9999848031710253382, -0.005512562950849705760 ) ) ;
#13579=ORIENTED_EDGE ( 'NONE', *, *, #10972, .T. ) ;
#13584=AXIS2_PLACEMENT_3D ( 'NONE', #14713, #22450, #3073 ) ;
#13601=EDGE_CURVE ( 'NONE', #11233, #18558, #5632, .T. ) ;
#13633=EDGE_CURVE ( 'NONE', #19439, #5742, #18537, .T. ) ;
#13662=CARTESIAN_POINT ( 'NONE',  ( -61.67516800463454985, 127.4153035195788561, 257.6560318593087686 ) ) ;
#13666=LINE ( 'NONE', #17454, #4068 ) ;
#13669=CARTESIAN_POINT ( 'NONE',  ( -56.88982296092818558, 126.2575686056375304, 47.57983110662539161 ) ) ;
#13690=DIRECTION ( 'NONE',  ( 0.01111468050521610164, -0.5103046645782707280, 0.8599218645824314722 ) ) ;
#13691=LINE ( 'NONE', #20673, #20075 ) ;
#13696=DIRECTION ( 'NONE',  ( -0.9999164797902017066, -2.045740421681430110E-15, 0.01292414190464156835 ) ) ;
#13730=ORIENTED_EDGE ( 'NONE', *, *, #19183, .T. ) ;
#13731=EDGE_CURVE ( 'NONE', #3377, #16056, #11543, .T. ) ;
#13742=CARTESIAN_POINT ( 'NONE',  ( -55.33894950108811628, 126.9191314136040063, 167.5679852142817197 ) ) ;
#13755=VERTEX_POINT ( 'NONE', #20761 ) ;
#13758=ADVANCED_FACE ( 'NONE', ( #19270 ), #10326, .F. ) ;
#13766=EDGE_CURVE ( 'NONE', #20506, #12670, #14493, .T. ) ;
#13782=EDGE_CURVE ( 'NONE', #12812, #11335, #19942, .T. ) ;
#13789=VECTOR ( 'NONE', #7805, 1000.000000000000227 ) ;
#13793=CARTESIAN_POINT ( 'NONE',  ( -19.00623411919002592, 140.4227465520235967, 77.01503843080352851 ) ) ;
#13799=DIRECTION ( 'NONE',  ( -0.01292394549866632963, -0.005513023399716958026, -0.9999012842304692006 ) ) ;
#13807=ORIENTED_EDGE ( 'NONE', *, *, #14353, .T. ) ;
#13812=ORIENTED_EDGE ( 'NONE', *, *, #6514, .F. ) ;
#13815=CARTESIAN_POINT ( 'NONE',  ( -56.92213282467484703, 126.2437860471382294, 45.08007789604923232 ) ) ;
#13859=EDGE_CURVE ( 'NONE', #1058, #12670, #7302, .T. ) ;
#13860=DIRECTION ( 'NONE',  ( 0.01292394549866738782, 0.005513023399720700692, 0.9999012842304693116 ) ) ;
#13885=ORIENTED_EDGE ( 'NONE', *, *, #3172, .F. ) ;
#13889=VECTOR ( 'NONE', #4401, 1000.000000000000227 ) ;
#13907=DIRECTION ( 'NONE',  ( -0.01292394549866731669, -0.005513023399719711899, -0.9999012842304692006 ) ) ;
#13929=AXIS2_PLACEMENT_3D ( 'NONE', #21674, #5965, #13106 ) ;
#13948=VECTOR ( 'NONE', #20294, 1000.000000000000000 ) ;
#13954=CARTESIAN_POINT ( 'NONE',  ( -61.67972807482614428, 191.4143309225244707, 257.3032278304543183 ) ) ;
#13957=AXIS2_PLACEMENT_3D ( 'NONE', #191, #13972, #12377 ) ;
#13961=VECTOR ( 'NONE', #4019, 1000.000000000000000 ) ;
#13972=DIRECTION ( 'NONE',  ( 7.125109674364534776E-05, -0.9999848031710252272, 0.005512562950849704893 ) ) ;
#13974=VECTOR ( 'NONE', #6986, 1000.000000000000000 ) ;
#13980=CIRCLE ( 'NONE', #4062, 2.499999999999988010 ) ;
#13992=DIRECTION ( 'NONE',  ( -0.01292394549866632963, -0.005513023399716958026, -0.9999012842304692006 ) ) ;
#13993=EDGE_CURVE ( 'NONE', #1614, #1930, #16688, .T. ) ;
#14015=CARTESIAN_POINT ( 'NONE',  ( 48.31072223536619958, 166.8507685304810764, 256.0170097695137201 ) ) ;
#14038=VECTOR ( 'NONE', #14702, 1000.000000000000114 ) ;
#14041=ORIENTED_EDGE ( 'NONE', *, *, #2422, .F. ) ;
#14059=FACE_OUTER_BOUND ( 'NONE', #301, .T. ) ;
#14066=CARTESIAN_POINT ( 'NONE',  ( -56.88982296092818558, 126.2575686056375304, 47.57983110662539161 ) ) ;
#14068=EDGE_LOOP ( 'NONE', ( #9490, #17389, #19099 ) ) ;
#14080=FACE_OUTER_BOUND ( 'NONE', #7247, .T. ) ;
#14082=DIRECTION ( 'NONE',  ( 7.125109674364534776E-05, -0.9999848031710252272, 0.005512562950849704893 ) ) ;
#14085=CYLINDRICAL_SURFACE ( 'NONE', #7845, 3.399999999999986144 ) ;
#14096=ORIENTED_EDGE ( 'NONE', *, *, #9360, .F. ) ;
#14099=ORIENTED_EDGE ( 'NONE', *, *, #11734, .F. ) ;
#14157=EDGE_CURVE ( 'NONE', #16867, #1653, #10800, .T. ) ;
#14189=EDGE_CURVE ( 'NONE', #20596, #12054, #19269, .T. ) ;
#14191=ORIENTED_EDGE ( 'NONE', *, *, #18375, .F. ) ;
#14195=ORIENTED_EDGE ( 'NONE', *, *, #14189, .T. ) ;
#14209=ORIENTED_EDGE ( 'NONE', *, *, #2341, .T. ) ;
#14241=AXIS2_PLACEMENT_3D ( 'NONE', #11963, #15313, #13799 ) ;
#14254=ORIENTED_EDGE ( 'NONE', *, *, #16541, .T. ) ;
#14257=FACE_BOUND ( 'NONE', #21338, .T. ) ;
#14273=DIRECTION ( 'NONE',  ( 7.125109674381880655E-05, -0.9999848031710253382, 0.005512562950849702291 ) ) ;
#14281=DIRECTION ( 'NONE',  ( -0.01292394549866738782, -0.005513023399720700692, -0.9999012842304693116 ) ) ;
#14299=ORIENTED_EDGE ( 'NONE', *, *, #12045, .F. ) ;
#14336=AXIS2_PLACEMENT_3D ( 'NONE', #22402, #10149, #1320 ) ;
#14353=EDGE_CURVE ( 'NONE', #5961, #3219, #14506, .T. ) ;
#14382=CARTESIAN_POINT ( 'NONE',  ( -41.14926644985963122, 168.6907664596094776, 35.14123791416483300 ) ) ;
#14400=CARTESIAN_POINT ( 'NONE',  ( -64.65223553951962288, 190.1463355405887228, 27.32593245744643795 ) ) ;
#14401=ORIENTED_EDGE ( 'NONE', *, *, #4206, .F. ) ;
#14402=CARTESIAN_POINT ( 'NONE',  ( 49.13077451860386446, 168.8134312302534283, 56.22586871687502708 ) ) ;
#14406=ORIENTED_EDGE ( 'NONE', *, *, #1103, .F. ) ;
#14419=EDGE_CURVE ( 'NONE', #4965, #13170, #11433, .T. ) ;
#14433=CARTESIAN_POINT ( 'NONE',  ( -49.64993871177497198, 140.1470898690141098, 27.40669857513504226 ) ) ;
#14444=AXIS2_PLACEMENT_3D ( 'NONE', #8002, #4441, #2403 ) ;
#14450=EDGE_LOOP ( 'NONE', ( #17872, #21750 ) ) ;
#14458=CARTESIAN_POINT ( 'NONE',  ( 68.30941429790007646, 191.4143309225247549, 255.6230893828509352 ) ) ;
#14484=ORIENTED_EDGE ( 'NONE', *, *, #798, .T. ) ;
#14493=CIRCLE ( 'NONE', #21053, 2.499999999999988010 ) ;
#14506=CIRCLE ( 'NONE', #7513, 10.00000000000000711 ) ;
#14513=DIRECTION ( 'NONE',  ( 7.125109674364536131E-05, -0.9999848031710253382, 0.005512562950849705760 ) ) ;
#14519=ORIENTED_EDGE ( 'NONE', *, *, #4272, .F. ) ;
#14528=ORIENTED_EDGE ( 'NONE', *, *, #15872, .F. ) ;
#14541=DIRECTION ( 'NONE',  ( -0.9999164797902015955, -2.219203356785933794E-15, 0.01292414190464157009 ) ) ;
#14551=LINE ( 'NONE', #4285, #22382 ) ;
#14570=ORIENTED_EDGE ( 'NONE', *, *, #19388, .T. ) ;
#14588=EDGE_CURVE ( 'NONE', #4299, #18381, #5656, .T. ) ;
#14596=EDGE_LOOP ( 'NONE', ( #6921, #20798, #13730 ) ) ;
#14597=DIRECTION ( 'NONE',  ( -0.01292394549866738608, -0.005513023399720699824, -0.9999012842304692006 ) ) ;
#14604=ORIENTED_EDGE ( 'NONE', *, *, #21469, .T. ) ;
#14608=DIRECTION ( 'NONE',  ( 0.01292394549866738782, 0.005513023399720700692, 0.9999012842304693116 ) ) ;
#14628=DIRECTION ( 'NONE',  ( 7.125109674364534776E-05, -0.9999848031710252272, 0.005512562950849704893 ) ) ;
#14632=DIRECTION ( 'NONE',  ( 7.125109674364534776E-05, -0.9999848031710252272, 0.005512562950849704893 ) ) ;
#14634=CARTESIAN_POINT ( 'NONE',  ( 59.65144567478507298, 126.9191314136042479, 166.0817088952479139 ) ) ;
#14638=DIRECTION ( 'NONE',  ( -0.01292394549866632963, -0.005513023399716958026, -0.9999012842304692006 ) ) ;
#14639=AXIS2_PLACEMENT_3D ( 'NONE', #19578, #5674, #16055 ) ;
#14643=EDGE_LOOP ( 'NONE', ( #14874, #18238, #454 ) ) ;
#14658=VECTOR ( 'NONE', #132, 999.9999999999998863 ) ;
#14667=ORIENTED_EDGE ( 'NONE', *, *, #7101, .T. ) ;
#14683=LINE ( 'NONE', #22094, #15579 ) ;
#14693=FACE_BOUND ( 'NONE', #129, .T. ) ;
#14702=DIRECTION ( 'NONE',  ( -7.125109674364534776E-05, 0.9999848031710252272, -0.005512562950849704026 ) ) ;
#14713=CARTESIAN_POINT ( 'NONE',  ( 0.9903141991953918755, 165.4223666312992975, 76.61874151893944429 ) ) ;
#14728=ORIENTED_EDGE ( 'NONE', *, *, #6401, .F. ) ;
#14772=DIRECTION ( 'NONE',  ( 7.125109674364534776E-05, -0.9999848031710252272, 0.005512562950849704893 ) ) ;
#14795=CARTESIAN_POINT ( 'NONE',  ( -8.877829866301334860, 140.4778767860208291, 86.88480985406179968 ) ) ;
#14806=VECTOR ( 'NONE', #16328, 999.9999999999998863 ) ;
#14826=AXIS2_PLACEMENT_3D ( 'NONE', #1559, #3499, #20948 ) ;
#14833=DIRECTION ( 'NONE',  ( 7.125109674364536131E-05, -0.9999848031710253382, 0.005512562950849705760 ) ) ;
#14841=AXIS2_PLACEMENT_3D ( 'NONE', #10256, #17058, #1321 ) ;
#14860=EDGE_CURVE ( 'NONE', #10313, #1614, #8154, .T. ) ;
#14874=ORIENTED_EDGE ( 'NONE', *, *, #7971, .F. ) ;
#14875=VECTOR ( 'NONE', #17759, 1000.000000000000114 ) ;
#14910=ADVANCED_FACE ( 'NONE', ( #3303 ), #3646, .F. ) ;
#14934=AXIS2_PLACEMENT_3D ( 'NONE', #3195, #12063, #1497 ) ;
#14944=EDGE_LOOP ( 'NONE', ( #17118, #22162, #12229 ) ) ;
#14969=DIRECTION ( 'NONE',  ( -0.01104128644981183967, -0.5197558313507629757, -0.8542435049623791077 ) ) ;
#14980=EDGE_CURVE ( 'NONE', #1058, #4221, #20621, .T. ) ;
#14985=LINE ( 'NONE', #4612, #1895 ) ;
#14987=DIRECTION ( 'NONE',  ( -7.125109674364534776E-05, 0.9999848031710252272, -0.005512562950849704893 ) ) ;
#15003=CARTESIAN_POINT ( 'NONE',  ( -41.67747345744867715, 165.9786531560170033, 257.1849355913340673 ) ) ;
#15006=DIRECTION ( 'NONE',  ( -7.125109674364534776E-05, 0.9999848031710252272, -0.005512562950849704893 ) ) ;
#15028=ORIENTED_EDGE ( 'NONE', *, *, #1414, .F. ) ;
#15041=DIRECTION ( 'NONE',  ( 0.9999164797902015955, 2.044556590511377167E-15, -0.01292414190464178173 ) ) ;
#15048=CARTESIAN_POINT ( 'NONE',  ( -41.14926644985963122, 168.6907664596094776, 35.14123791416483300 ) ) ;
#15050=ORIENTED_EDGE ( 'NONE', *, *, #16541, .F. ) ;
#15053=FACE_OUTER_BOUND ( 'NONE', #22141, .T. ) ;
#15084=FACE_OUTER_BOUND ( 'NONE', #1962, .T. ) ;
#15131=AXIS2_PLACEMENT_3D ( 'NONE', #3827, #3484, #17868 ) ;
#15132=EDGE_CURVE ( 'NONE', #11414, #19968, #16426, .T. ) ;
#15154=EDGE_LOOP ( 'NONE', ( #13325, #18268, #17821 ) ) ;
#15156=VECTOR ( 'NONE', #11953, 1000.000000000000000 ) ;
#15165=CARTESIAN_POINT ( 'NONE',  ( 58.87469064627514825, 145.0902203831571740, 105.9856375662876218 ) ) ;
#15173=ORIENTED_EDGE ( 'NONE', *, *, #11447, .T. ) ;
#15176=LINE ( 'NONE', #22128, #21102 ) ;
#15180=DIRECTION ( 'NONE',  ( -0.01292394549866738608, -0.005513023399720699824, -0.9999012842304692006 ) ) ;
#15183=CARTESIAN_POINT ( 'NONE',  ( 48.84321673125851504, 168.6907664596096765, 33.97806514274709144 ) ) ;
#15200=VERTEX_POINT ( 'NONE', #18802 ) ;
#15204=DIRECTION ( 'NONE',  ( -7.125109674381882011E-05, 0.9999848031710253382, -0.005512562950849702291 ) ) ;
#15206=FACE_BOUND ( 'NONE', #9008, .T. ) ;
#15213=ORIENTED_EDGE ( 'NONE', *, *, #1901, .T. ) ;
#15220=ORIENTED_EDGE ( 'NONE', *, *, #656, .F. ) ;
#15242=ORIENTED_EDGE ( 'NONE', *, *, #4272, .T. ) ;
#15245=ORIENTED_EDGE ( 'NONE', *, *, #19390, .T. ) ;
#15289=EDGE_CURVE ( 'NONE', #11233, #9564, #5447, .T. ) ;
#15297=PRODUCT_CONTEXT ( 'NONE', #12043, 'mechanical' ) ;
#15313=DIRECTION ( 'NONE',  ( 7.125109674364534776E-05, -0.9999848031710252272, 0.005512562950849704893 ) ) ;
#15347=EDGE_LOOP ( 'NONE', ( #4606, #18768 ) ) ;
#15360=DIRECTION ( 'NONE',  ( -0.01292394549866738608, -0.005513023399720699824, -0.9999012842304692006 ) ) ;
#15373=VERTEX_POINT ( 'NONE', #10526 ) ;
#15380=DIRECTION ( 'NONE',  ( -0.01292394549866738608, -0.005513023399720699824, -0.9999012842304692006 ) ) ;
#15393=EDGE_CURVE ( 'NONE', #18381, #6677, #7348, .T. ) ;
#15409=FACE_OUTER_BOUND ( 'NONE', #9950, .T. ) ;
#15425=FACE_OUTER_BOUND ( 'NONE', #13402, .T. ) ;
#15453=ORIENTED_EDGE ( 'NONE', *, *, #18882, .T. ) ;
#15466=ORIENTED_EDGE ( 'NONE', *, *, #380, .F. ) ;
#15520=CARTESIAN_POINT ( 'NONE',  ( 21.11681448353495938, 180.4772689128619163, 86.27658307888856370 ) ) ;
#15524=CARTESIAN_POINT ( 'NONE',  ( -56.08207636726148593, 126.6021325681200551, 110.0736613710297007 ) ) ;
#15534=AXIS2_PLACEMENT_3D ( 'NONE', #19879, #4145, #18189 ) ;
#15535=FACE_BOUND ( 'NONE', #1306, .T. ) ;
#15536=DIRECTION ( 'NONE',  ( 7.125109674364534776E-05, -0.9999848031710252272, 0.005512562950849704893 ) ) ;
#15552=CARTESIAN_POINT ( 'NONE',  ( 59.65012737619518646, 145.4210017871403977, 165.9797146201158000 ) ) ;
#15558=EDGE_CURVE ( 'NONE', #6907, #18220, #8868, .T. ) ;
#15579=VECTOR ( 'NONE', #16750, 1000.000000000000114 ) ;
#15597=VERTEX_POINT ( 'NONE', #21264 ) ;
#15615=CARTESIAN_POINT ( 'NONE',  ( 45.73105848731719192, 168.8134312302534283, 56.26981079935081453 ) ) ;
#15640=DIRECTION ( 'NONE',  ( 0.9999164797902015955, 2.175835928943913463E-15, -0.01292414190464156835 ) ) ;
#15649=CYLINDRICAL_SURFACE ( 'NONE', #18889, 3.399999999999986144 ) ;
#15679=FACE_OUTER_BOUND ( 'NONE', #3613, .T. ) ;
#15710=DIRECTION ( 'NONE',  ( 7.125109674364534776E-05, -0.9999848031710252272, 0.005512562950849704893 ) ) ;
#15717=ADVANCED_FACE ( 'NONE', ( #18291 ), #377, .F. ) ;
#15721=ORIENTED_EDGE ( 'NONE', *, *, #6401, .T. ) ;
#15723=DIRECTION ( 'NONE',  ( -0.01292394549866632963, -0.005513023399716958026, -0.9999012842304692006 ) ) ;
#15733=COLOUR_RGB ( '', 0.66274510, 0.83137255, 0.94901961) ;
#15750=LINE ( 'NONE', #13793, #19934 ) ;
#15794=CYLINDRICAL_SURFACE ( 'NONE', #15131, 2.499999999999988010 ) ;
#15808=EDGE_CURVE ( 'NONE', #19674, #8677, #7726, .T. ) ;
#15813=VECTOR ( 'NONE', #11991, 999.9999999999998863 ) ;
#15815=DIRECTION ( 'NONE',  ( -0.01292394549866632963, -0.005513023399716958026, -0.9999012842304692006 ) ) ;
#15840=CARTESIAN_POINT ( 'NONE',  ( -41.99143391042890272, 165.8447256859541596, 232.8944075815348924 ) ) ;
#15847=EDGE_LOOP ( 'NONE', ( #2505, #6492, #12786, #10649 ) ) ;
#15865=CARTESIAN_POINT ( 'NONE',  ( -38.27775742616200461, 165.9786531560170033, 257.1409935088582870 ) ) ;
#15872=EDGE_CURVE ( 'NONE', #6677, #3377, #13666, .T. ) ;
#15880=ORIENTED_EDGE ( 'NONE', *, *, #18021, .F. ) ;
#15899=DIRECTION ( 'NONE',  ( -0.01292394549866632963, -0.005513023399716958026, -0.9999012842304692006 ) ) ;
#15909=ORIENTED_EDGE ( 'NONE', *, *, #682, .T. ) ;
#15924=ORIENTED_EDGE ( 'NONE', *, *, #13859, .F. ) ;
#15932=FACE_OUTER_BOUND ( 'NONE', #12601, .T. ) ;
#15938=CARTESIAN_POINT ( 'NONE',  ( -55.34016076973275489, 143.9188730675114414, 167.4742716441172377 ) ) ;
#15949=CONICAL_SURFACE ( 'NONE', #17783, 2.499999999999988010, 1.029744258676651425 ) ;
#15995=DIRECTION ( 'NONE',  ( 0.01292394549866738782, 0.005513023399720701559, 0.9999012842304693116 ) ) ;
#16019=DIRECTION ( 'NONE',  ( -0.01292394549866632963, -0.005513023399716958026, -0.9999012842304692006 ) ) ;
#16040=LINE ( 'NONE', #21278, #5921 ) ;
#16043=LINE ( 'NONE', #14433, #17942 ) ;
#16055=DIRECTION ( 'NONE',  ( -0.9999164797902015955, 0.000000000000000000, 0.01292414190464162733 ) ) ;
#16056=VERTEX_POINT ( 'NONE', #12476 ) ;
#16079=ORIENTED_EDGE ( 'NONE', *, *, #666, .F. ) ;
#16085=CIRCLE ( 'NONE', #14241, 2.499999999999988010 ) ;
#16086=DIRECTION ( 'NONE',  ( 7.125109674364534776E-05, -0.9999848031710252272, 0.005512562950849704893 ) ) ;
#16111=CARTESIAN_POINT ( 'NONE',  ( -56.88982296092818558, 126.2575686056375304, 47.57983110662539161 ) ) ;
#16138=VECTOR ( 'NONE', #20193, 1000.000000000000000 ) ;
#16174=ORIENTED_EDGE ( 'NONE', *, *, #2638, .F. ) ;
#16195=CARTESIAN_POINT ( 'NONE',  ( 58.84248781247372762, 143.5743091050291298, 103.4941650606791512 ) ) ;
#16205=VECTOR ( 'NONE', #2052, 999.9999999999998863 ) ;
#16219=CARTESIAN_POINT ( 'NONE',  ( -47.94869851243297632, 168.6907664596094776, 35.22912207911639371 ) ) ;
#16222=VECTOR ( 'NONE', #4511, 1000.000000000000114 ) ;
#16229=ORIENTED_EDGE ( 'NONE', *, *, #15393, .F. ) ;
#16237=VERTEX_POINT ( 'NONE', #6027 ) ;
#16241=LINE ( 'NONE', #5861, #904 ) ;
#16249=AXIS2_PLACEMENT_3D ( 'NONE', #7121, #15995, #21015 ) ;
#16252=FACE_OUTER_BOUND ( 'NONE', #16735, .T. ) ;
#16280=EDGE_CURVE ( 'NONE', #12054, #19674, #14551, .T. ) ;
#16292=ORIENTED_EDGE ( 'NONE', *, *, #19931, .F. ) ;
#16296=FACE_OUTER_BOUND ( 'NONE', #2290, .T. ) ;
#16302=DIRECTION ( 'NONE',  ( -0.01292394549866738608, -0.005513023399720699824, -0.9999012842304692006 ) ) ;
#16307=CARTESIAN_POINT ( 'NONE',  ( 58.13288207869166513, 126.2713511641370445, 48.59330799816777358 ) ) ;
#16313=AXIS2_PLACEMENT_3D ( 'NONE', #7883, #18233, #4538 ) ;
#16314=EDGE_LOOP ( 'NONE', ( #14528, #16229, #17168, #19129 ) ) ;
#16323=ORIENTED_EDGE ( 'NONE', *, *, #91, .T. ) ;
#16328=DIRECTION ( 'NONE',  ( 7.125109674364536131E-05, -0.9999848031710253382, 0.005512562950849705760 ) ) ;
#16360=CARTESIAN_POINT ( 'NONE',  ( 20.98757502854828516, 180.4221386788647123, 76.27757023658386970 ) ) ;
#16383=ORIENTED_EDGE ( 'NONE', *, *, #17994, .F. ) ;
#16418=EDGE_CURVE ( 'NONE', #13170, #20174, #20817, .T. ) ;
#16426=LINE ( 'NONE', #789, #14038 ) ;
#16467=CARTESIAN_POINT ( 'NONE',  ( 58.84248781247372762, 143.5743091050291298, 103.4941650606791370 ) ) ;
#16487=CYLINDRICAL_SURFACE ( 'NONE', #10044, 2.499999999999988010 ) ;
#16495=ORIENTED_EDGE ( 'NONE', *, *, #569, .F. ) ;
#16532=ORIENTED_EDGE ( 'NONE', *, *, #1716, .T. ) ;
#16535=PRODUCT ( 'Moving Jaw', 'Moving Jaw', '', ( #15297 ) ) ;
#16541=EDGE_CURVE ( 'NONE', #6907, #16237, #10842, .T. ) ;
#16558=ADVANCED_FACE ( 'NONE', ( #15679 ), #15794, .F. ) ;
#16577=ORIENTED_EDGE ( 'NONE', *, *, #14419, .T. ) ;
#16608=DIRECTION ( 'NONE',  ( -0.01292394549866632963, -0.005513023399716958026, -0.9999012842304692006 ) ) ;
#16611=DIRECTION ( 'NONE',  ( 0.01292394549866738782, 0.005513023399720700692, 0.9999012842304693116 ) ) ;
#16627=EDGE_LOOP ( 'NONE', ( #11120, #17870, #1126 ) ) ;
#16632=AXIS2_PLACEMENT_3D ( 'NONE', #21694, #9775, #2430 ) ;
#16653=EDGE_LOOP ( 'NONE', ( #13885, #18295, #18921, #11475 ) ) ;
#16668=DIRECTION ( 'NONE',  ( -7.125109674381882011E-05, 0.9999848031710253382, -0.005512562950849702291 ) ) ;
#16688=CIRCLE ( 'NONE', #13373, 3.399999999999986144 ) ;
#16734=DIRECTION ( 'NONE',  ( 0.01292394549866738608, 0.005513023399720699824, 0.9999012842304692006 ) ) ;
#16735=EDGE_LOOP ( 'NONE', ( #3016, #20638, #4527, #16739 ) ) ;
#16739=ORIENTED_EDGE ( 'NONE', *, *, #21404, .F. ) ;
#16741=CARTESIAN_POINT ( 'NONE',  ( 42.04378466868516995, 168.6907664596096765, 34.06594930769865925 ) ) ;
#16750=DIRECTION ( 'NONE',  ( -0.01104128644981183967, -0.5197558313507629757, -0.8542435049623791077 ) ) ;
#16756=VERTEX_POINT ( 'NONE', #22048 ) ;
#16773=VECTOR ( 'NONE', #3909, 1000.000000000000114 ) ;
#16774=LINE ( 'NONE', #1142, #8232 ) ;
#16783=ADVANCED_BREP_SHAPE_REPRESENTATION ( '', ( #1836, #6292 ), #11807 ) ;
#16784=SHAPE_DEFINITION_REPRESENTATION ( #17686, #10182 ) ;
#16792=DIRECTION ( 'NONE',  ( -0.01292394549866738608, -0.005513023399720699824, -0.9999012842304692006 ) ) ;
#16818=CARTESIAN_POINT ( 'NONE',  ( 68.30941429790007646, 191.4143309225247549, 255.6230893828509352 ) ) ;
#16828=CIRCLE ( 'NONE', #14639, 3.399999999999986144 ) ;
#16856=DIRECTION ( 'NONE',  ( 0.01292394549866738782, 0.005513023399720700692, 0.9999012842304693116 ) ) ;
#16867=VERTEX_POINT ( 'NONE', #16219 ) ;
#16904=ORIENTED_EDGE ( 'NONE', *, *, #6514, .T. ) ;
#16912=DIRECTION ( 'NONE',  ( 0.8504393858994485633, -0.002839416958724378954, -0.5260653843604455870 ) ) ;
#16930=CIRCLE ( 'NONE', #19826, 2.499999999999988010 ) ;
#16941=FACE_OUTER_BOUND ( 'NONE', #19334, .T. ) ;
#16988=ORIENTED_EDGE ( 'NONE', *, *, #10201, .T. ) ;
#17036=AXIS2_PLACEMENT_3D ( 'NONE', #10563, #5261, #17583 ) ;
#17058=DIRECTION ( 'NONE',  ( 0.01292394549866738608, 0.005513023399720699824, 0.9999012842304692006 ) ) ;
#17065=DIRECTION ( 'NONE',  ( -0.01292394549866632963, -0.005513023399716958026, -0.9999012842304692006 ) ) ;
#17066=CARTESIAN_POINT ( 'NONE',  ( -61.67972807482614428, 191.4143309225244707, 257.3032278304543183 ) ) ;
#17081=VERTEX_POINT ( 'NONE', #9975 ) ;
#17098=FACE_OUTER_BOUND ( 'NONE', #19576, .T. ) ;
#17116=CARTESIAN_POINT ( 'NONE',  ( 58.13167081004702652, 143.2710928180444796, 48.49959442800333420 ) ) ;
#17118=ORIENTED_EDGE ( 'NONE', *, *, #2341, .F. ) ;
#17120=ORIENTED_EDGE ( 'NONE', *, *, #22408, .T. ) ;
#17122=DIRECTION ( 'NONE',  ( -0.01292394549866738782, -0.005513023399720700692, -0.9999012842304693116 ) ) ;
#17133=FACE_OUTER_BOUND ( 'NONE', #21354, .T. ) ;
#17162=DIRECTION ( 'NONE',  ( 0.01292394549866738782, 0.005513023399720700692, 0.9999012842304693116 ) ) ;
#17168=ORIENTED_EDGE ( 'NONE', *, *, #21404, .T. ) ;
#17176=FACE_OUTER_BOUND ( 'NONE', #19738, .T. ) ;
#17179=FACE_OUTER_BOUND ( 'NONE', #4452, .T. ) ;
#17200=EDGE_CURVE ( 'NONE', #4784, #9640, #13484, .T. ) ;
#17213=ADVANCED_FACE ( 'NONE', ( #7418 ), #9804, .F. ) ;
#17224=DIRECTION ( 'NONE',  ( 0.01292394549866738608, 0.005513023399720699824, 0.9999012842304692006 ) ) ;
#17225=VERTEX_POINT ( 'NONE', #9249 ) ;
#17263=CYLINDRICAL_SURFACE ( 'NONE', #20305, 2.499999999999988010 ) ;
#17310=EDGE_CURVE ( 'NONE', #5640, #15200, #21602, .T. ) ;
#17336=ORIENTED_EDGE ( 'NONE', *, *, #9407, .F. ) ;
#17354=DIRECTION ( 'NONE',  ( 7.125109674364534776E-05, -0.9999848031710252272, 0.005512562950849704893 ) ) ;
#17389=ORIENTED_EDGE ( 'NONE', *, *, #7971, .T. ) ;
#17407=ADVANCED_FACE ( 'NONE', ( #8724 ), #12112, .F. ) ;
#17434=VECTOR ( 'NONE', #12343, 999.9999999999998863 ) ;
#17454=CARTESIAN_POINT ( 'NONE',  ( 59.68375553853174154, 126.9329139721035489, 168.5814621058240732 ) ) ;
#17461=CARTESIAN_POINT ( 'NONE',  ( 48.31072223536619958, 166.8507685304810764, 256.0170097695137201 ) ) ;
#17464=DIRECTION ( 'NONE',  ( -0.01292394549866632963, -0.005513023399716958026, -0.9999012842304692006 ) ) ;
#17466=CARTESIAN_POINT ( 'NONE',  ( -47.94869851243297632, 168.6907664596094776, 35.22912207911639371 ) ) ;
#17486=ADVANCED_FACE ( 'NONE', ( #4643 ), #11562, .F. ) ;
#17495=CYLINDRICAL_SURFACE ( 'NONE', #13143, 3.399999999999986144 ) ;
#17498=EDGE_LOOP ( 'NONE', ( #3157, #200, #7088, #12388 ) ) ;
#17505=DIRECTION ( 'NONE',  ( 7.125109674364536131E-05, -0.9999848031710253382, 0.005512562950849705760 ) ) ;
#17508=DIRECTION ( 'NONE',  ( -0.9999164797902015955, -2.044556590511377167E-15, 0.01292414190464178346 ) ) ;
#17532=EDGE_LOOP ( 'NONE', ( #14401, #3973, #21795, #10841 ) ) ;
#17534=CONICAL_SURFACE ( 'NONE', #3186, 3.399999999999986144, 1.029744258676653201 ) ;
#17547=DIRECTION ( 'NONE',  ( 7.125109674364536131E-05, -0.9999848031710253382, 0.005512562950849705760 ) ) ;
#17573=CARTESIAN_POINT ( 'NONE',  ( 59.65023440614042727, 143.9188730675116688, 165.9879953250834603 ) ) ;
#17575=ORIENTED_EDGE ( 'NONE', *, *, #20428, .F. ) ;
#17583=DIRECTION ( 'NONE',  ( -0.01292394549866632963, -0.005513023399716958026, -0.9999012842304692006 ) ) ;
#17589=DIRECTION ( 'NONE',  ( 0.01292394549866738782, 0.005513023399720700692, 0.9999012842304693116 ) ) ;
#17599=EDGE_CURVE ( 'NONE', #4965, #2088, #18429, .T. ) ;
#17606=CONICAL_SURFACE ( 'NONE', #7684, 2.499999999999988010, 1.029744258676651425 ) ;
#17618=DIRECTION ( 'NONE',  ( -0.01292394549866632963, -0.005513023399716958026, -0.9999012842304692006 ) ) ;
#17621=CARTESIAN_POINT ( 'NONE',  ( -49.64892827247505380, 126.1473081376431367, 27.48487435773119714 ) ) ;
#17658=VERTEX_POINT ( 'NONE', #21398 ) ;
#17686=PRODUCT_DEFINITION_SHAPE ( 'NONE', 'NONE',  #20803 ) ;
#17699=CYLINDRICAL_SURFACE ( 'NONE', #2966, 3.399999999999992806 ) ;
#17759=DIRECTION ( 'NONE',  ( -0.01104128644981183967, -0.5197558313507629757, -0.8542435049623791077 ) ) ;
#17764=VECTOR ( 'NONE', #1235, 1000.000000000000227 ) ;
#17783=AXIS2_PLACEMENT_3D ( 'NONE', #10425, #12272, #6960 ) ;
#17804=ADVANCED_FACE ( 'NONE', ( #16941 ), #6604, .F. ) ;
#17821=ORIENTED_EDGE ( 'NONE', *, *, #569, .T. ) ;
#17850=ORIENTED_EDGE ( 'NONE', *, *, #78, .F. ) ;
#17868=DIRECTION ( 'NONE',  ( -0.01292394549866632963, -0.005513023399716958026, -0.9999012842304692006 ) ) ;
#17870=ORIENTED_EDGE ( 'NONE', *, *, #11734, .T. ) ;
#17872=ORIENTED_EDGE ( 'NONE', *, *, #1387, .F. ) ;
#17888=ORIENTED_EDGE ( 'NONE', *, *, #452, .F. ) ;
#17903=AXIS2_PLACEMENT_3D ( 'NONE', #7937, #14632, #715 ) ;
#17929=ORIENTED_EDGE ( 'NONE', *, *, #3822, .F. ) ;
#17934=EDGE_CURVE ( 'NONE', #15373, #13257, #11727, .T. ) ;
#17942=VECTOR ( 'NONE', #16611, 999.9999999999998863 ) ;
#17980=VECTOR ( 'NONE', #18166, 1000.000000000000227 ) ;
#17984=DIRECTION ( 'NONE',  ( 0.01292394549866738608, 0.005513023399720699824, 0.9999012842304692006 ) ) ;
#17992=DIRECTION ( 'NONE',  ( 7.125109674364536131E-05, -0.9999848031710253382, 0.005512562950849705760 ) ) ;
#17994=EDGE_CURVE ( 'NONE', #9131, #9564, #2279, .T. ) ;
#18002=FILL_AREA_STYLE ('',( #1914 ) ) ;
#18005=CARTESIAN_POINT ( 'NONE',  ( -55.37247063347942344, 143.9050905090121546, 164.9745184335410784 ) ) ;
#18021=EDGE_CURVE ( 'NONE', #3219, #12722, #8486, .T. ) ;
#18054=DIRECTION ( 'NONE',  ( 7.125109674364534776E-05, -0.9999848031710252272, 0.005512562950849704893 ) ) ;
#18072=ORIENTED_EDGE ( 'NONE', *, *, #5269, .T. ) ;
#18078=VECTOR ( 'NONE', #22137, 999.9999999999998863 ) ;
#18094=ORIENTED_EDGE ( 'NONE', *, *, #676, .T. ) ;
#18098=CARTESIAN_POINT ( 'NONE',  ( 58.90710753996705762, 143.6018742220277318, 108.4936714818314698 ) ) ;
#18102=AXIS2_PLACEMENT_3D ( 'NONE', #1136, #21775, #19949 ) ;
#18141=ADVANCED_FACE ( 'NONE', ( #10350, #14257, #8948 ), #5617, .F. ) ;
#18145=CIRCLE ( 'NONE', #21746, 2.499999999999988010 ) ;
#18153=EDGE_CURVE ( 'NONE', #18558, #9131, #20895, .T. ) ;
#18166=DIRECTION ( 'NONE',  ( -0.9999164797902015955, -2.219203356785933794E-15, 0.01292414190464157009 ) ) ;
#18173=CARTESIAN_POINT ( 'NONE',  ( 23.31673526217817027, 141.4150907639734385, 256.4803039161023435 ) ) ;
#18174=ORIENTED_EDGE ( 'NONE', *, *, #11212, .F. ) ;
#18189=DIRECTION ( 'NONE',  ( -0.9999164797902015955, -2.045145117964614424E-15, 0.01292414190464167591 ) ) ;
#18192=EDGE_LOOP ( 'NONE', ( #13340, #19716, #8116, #20478 ) ) ;
#18205=CARTESIAN_POINT ( 'NONE',  ( 58.06705108255369652, 143.2435277010459060, 43.50008800685100141 ) ) ;
#18215=CARTESIAN_POINT ( 'NONE',  ( -56.89114125951807210, 144.7594389791736944, 47.47783683149325640 ) ) ;
#18220=VERTEX_POINT ( 'NONE', #12530 ) ;
#18225=CARTESIAN_POINT ( 'NONE',  ( -56.14790736339946164, 143.5743091050289024, 104.9804413797129286 ) ) ;
#18229=EDGE_CURVE ( 'NONE', #18675, #13755, #11143, .T. ) ;
#18233=DIRECTION ( 'NONE',  ( -0.01292394549866738608, -0.005513023399720699824, -0.9999012842304692006 ) ) ;
#18238=ORIENTED_EDGE ( 'NONE', *, *, #2105, .T. ) ;
#18256=VERTEX_POINT ( 'NONE', #21668 ) ;
#18260=LINE ( 'NONE', #9520, #20454 ) ;
#18265=CARTESIAN_POINT ( 'NONE',  ( -18.87699466420335170, 140.4778767860208006, 87.01405127310820831 ) ) ;
#18268=ORIENTED_EDGE ( 'NONE', *, *, #1377, .T. ) ;
#18281=CIRCLE ( 'NONE', #18648, 2.499999999999988010 ) ;
#18291=FACE_OUTER_BOUND ( 'NONE', #16314, .T. ) ;
#18295=ORIENTED_EDGE ( 'NONE', *, *, #9514, .T. ) ;
#18301=AXIS2_PLACEMENT_3D ( 'NONE', #15615, #10988, #12277 ) ;
#18313=LINE ( 'NONE', #9716, #13889 ) ;
#18335=AXIS2_PLACEMENT_3D ( 'NONE', #20076, #2300, #11148 ) ;
#18336=CARTESIAN_POINT ( 'NONE',  ( 50.34172219119072622, 140.1470953820377474, 26.11528428595510931 ) ) ;
#18356=ORIENTED_EDGE ( 'NONE', *, *, #2649, .F. ) ;
#18375=EDGE_CURVE ( 'NONE', #5742, #18256, #1021, .T. ) ;
#18381=VERTEX_POINT ( 'NONE', #11594 ) ;
#18429=LINE ( 'NONE', #2695, #6952 ) ;
#18434=CONICAL_SURFACE ( 'NONE', #21342, 2.499999999999988010, 1.029744258676651425 ) ;
#18442=AXIS2_PLACEMENT_3D ( 'NONE', #17461, #12169, #19154 ) ;
#18450=CARTESIAN_POINT ( 'NONE',  ( 10.98841023064628075, 180.4221386788646839, 76.40681165563029253 ) ) ;
#18451=ADVANCED_FACE ( 'NONE', ( #9472 ), #22058, .F. ) ;
#18455=ORIENTED_EDGE ( 'NONE', *, *, #9466, .T. ) ;
#18467=VERTEX_POINT ( 'NONE', #18225 ) ;
#18476=AXIS2_PLACEMENT_3D ( 'NONE', #4868, #11908, #3154 ) ;
#18487=ORIENTED_EDGE ( 'NONE', *, *, #20310, .T. ) ;
#18508=CARTESIAN_POINT ( 'NONE',  ( -44.26142469380095434, 168.8134312302532862, 57.43298357076854899 ) ) ;
#18537=LINE ( 'NONE', #8196, #502 ) ;
#18538=EDGE_CURVE ( 'NONE', #12722, #15597, #10371, .T. ) ;
#18554=EDGE_LOOP ( 'NONE', ( #9272, #5909, #18094, #4601 ) ) ;
#18558=VERTEX_POINT ( 'NONE', #4972 ) ;
#18605=DIRECTION ( 'NONE',  ( -0.9999164797902015955, 0.000000000000000000, 0.01292414190464162733 ) ) ;
#18614=DIRECTION ( 'NONE',  ( 0.01292394549866738608, 0.005513023399720699824, 0.9999012842304692006 ) ) ;
#18632=AXIS2_PLACEMENT_3D ( 'NONE', #3105, #6455, #1397 ) ;
#18636=CARTESIAN_POINT ( 'NONE',  ( -55.33894950108811628, 126.9191314136040063, 167.5679852142817197 ) ) ;
#18648=AXIS2_PLACEMENT_3D ( 'NONE', #6949, #15710, #8902 ) ;
#18653=EDGE_LOOP ( 'NONE', ( #15924, #15220, #16323, #1153 ) ) ;
#18659=VECTOR ( 'NONE', #4607, 1000.000000000000000 ) ;
#18670=AXIS2_PLACEMENT_3D ( 'NONE', #10745, #19236, #7403 ) ;
#18675=VERTEX_POINT ( 'NONE', #18173 ) ;
#18685=CARTESIAN_POINT ( 'NONE',  ( 65.44029839719591735, 190.1904397277867531, 33.64500428368677376 ) ) ;
#18689=ADVANCED_FACE ( 'NONE', ( #14080 ), #19105, .F. ) ;
#18724=CARTESIAN_POINT ( 'NONE',  ( -40.86170866251428180, 168.8134312302532862, 57.38904148829276863 ) ) ;
#18729=AXIS2_PLACEMENT_3D ( 'NONE', #753, #11087, #5904 ) ;
#18735=DIRECTION ( 'NONE',  ( 0.9999164797902017066, 2.219212769279110820E-15, -0.01292414190464157182 ) ) ;
#18748=DIRECTION ( 'NONE',  ( -0.01292394549866632963, -0.005513023399716958026, -0.9999012842304692006 ) ) ;
#18768=ORIENTED_EDGE ( 'NONE', *, *, #15808, .F. ) ;
#18785=DIRECTION ( 'NONE',  ( 0.01292394549866738782, 0.005513023399720700692, 0.9999012842304693116 ) ) ;
#18791=DIRECTION ( 'NONE',  ( 0.01292394549866738608, 0.005513023399720699824, 0.9999012842304692006 ) ) ;
#18794=AXIS2_PLACEMENT_3D ( 'NONE', #14458, #2376, #2248 ) ;
#18802=CARTESIAN_POINT ( 'NONE',  ( -55.37125936483477773, 126.9053488551047053, 165.0682320037055320 ) ) ;
#18810=CARTESIAN_POINT ( 'NONE',  ( 68.31397436809166379, 127.4153035195791119, 255.9758934117053570 ) ) ;
#18840=ORIENTED_EDGE ( 'NONE', *, *, #17599, .T. ) ;
#18847=ORIENTED_EDGE ( 'NONE', *, *, #22107, .F. ) ;
#18848=DIRECTION ( 'NONE',  ( -0.01292394549866738608, -0.005513023399720699824, -0.9999012842304692006 ) ) ;
#18867=CARTESIAN_POINT ( 'NONE',  ( -64.64902924016615771, 145.1470193978925636, 27.57399779023469932 ) ) ;
#18882=EDGE_CURVE ( 'NONE', #165, #4699, #3190, .T. ) ;
#18889=AXIS2_PLACEMENT_3D ( 'NONE', #6667, #19063, #5042 ) ;
#18892=ADVANCED_FACE ( 'NONE', ( #15409 ), #9634, .F. ) ;
#18910=EDGE_CURVE ( 'NONE', #3676, #5640, #20659, .T. ) ;
#18916=DIRECTION ( 'NONE',  ( 0.9999164797902015955, 2.045145117964614424E-15, -0.01292414190464167591 ) ) ;
#18921=ORIENTED_EDGE ( 'NONE', *, *, #2638, .T. ) ;
#18940=EDGE_LOOP ( 'NONE', ( #1732, #21032, #21149, #13052 ) ) ;
#18973=CARTESIAN_POINT ( 'NONE',  ( -56.89103422957282419, 143.2573102595449654, 47.48611753646095224 ) ) ;
#19063=DIRECTION ( 'NONE',  ( -0.01292394549866738608, -0.005513023399720699824, -0.9999012842304692006 ) ) ;
#19088=DIRECTION ( 'NONE',  ( 7.125109674364536131E-05, -0.9999848031710253382, 0.005512562950849705760 ) ) ;
#19099=ORIENTED_EDGE ( 'NONE', *, *, #1952, .T. ) ;
#19105=PLANE ( 'NONE',  #20257 ) ;
#19107=FACE_OUTER_BOUND ( 'NONE', #10376, .T. ) ;
#19112=PLANE ( 'NONE',  #22467 ) ;
#19120=VERTEX_POINT ( 'NONE', #15165 ) ;
#19129=ORIENTED_EDGE ( 'NONE', *, *, #1387, .T. ) ;
#19137=EDGE_LOOP ( 'NONE', ( #22020, #9241, #12434 ) ) ;
#19150=DIRECTION ( 'NONE',  ( 7.125109674364534776E-05, -0.9999848031710252272, 0.005512562950849704893 ) ) ;
#19154=DIRECTION ( 'NONE',  ( 0.9999164797902017066, 0.000000000000000000, -0.01292414190463751951 ) ) ;
#19183=EDGE_CURVE ( 'NONE', #11089, #12054, #855, .T. ) ;
#19216=ORIENTED_EDGE ( 'NONE', *, *, #10783, .F. ) ;
#19217=CARTESIAN_POINT ( 'NONE',  ( 59.61792454239376582, 143.9050905090123820, 163.4882421145073010 ) ) ;
#19230=DIRECTION ( 'NONE',  ( -0.01292394549866738782, -0.005513023399720700692, -0.9999012842304693116 ) ) ;
#19236=DIRECTION ( 'NONE',  ( 7.125109674364534776E-05, -0.9999848031710252272, 0.005512562950849704893 ) ) ;
#19247=PRESENTATION_STYLE_ASSIGNMENT (( #2129 ) ) ;
#19251=DIRECTION ( 'NONE',  ( -0.9999164797902015955, 0.000000000000000000, 0.01292414190464162733 ) ) ;
#19269=LINE ( 'NONE', #6978, #3458 ) ;
#19270=FACE_OUTER_BOUND ( 'NONE', #3923, .T. ) ;
#19274=CARTESIAN_POINT ( 'NONE',  ( 45.44350069997184249, 168.6907664596096765, 34.02200722522287180 ) ) ;
#19284=DIRECTION ( 'NONE',  ( 7.125109674364536131E-05, -0.9999848031710253382, 0.005512562950849705760 ) ) ;
#19316=ORIENTED_EDGE ( 'NONE', *, *, #4125, .T. ) ;
#19334=EDGE_LOOP ( 'NONE', ( #248, #4113, #12194 ) ) ;
#19348=EDGE_LOOP ( 'NONE', ( #9790, #5558, #6091, #19995 ) ) ;
#19351=LINE ( 'NONE', #3849, #6259 ) ;
#19359=MECHANICAL_DESIGN_GEOMETRIC_PRESENTATION_REPRESENTATION('',(#21196),#9460);
#19360=DIRECTION ( 'NONE',  ( 0.01292394549866738608, 0.005513023399720699824, 0.9999012842304692006 ) ) ;
#19388=EDGE_CURVE ( 'NONE', #1243, #21215, #19687, .T. ) ;
#19390=EDGE_CURVE ( 'NONE', #12054, #11089, #7072, .T. ) ;
#19405=DIRECTION ( 'NONE',  ( 0.9999164797902015955, 0.000000000000000000, -0.01292414190463754553 ) ) ;
#19418=FACE_OUTER_BOUND ( 'NONE', #12793, .T. ) ;
#19439=VERTEX_POINT ( 'NONE', #3861 ) ;
#19554=CARTESIAN_POINT ( 'NONE',  ( 65.34146690339817098, 126.1473081376433498, 25.99859803869739139 ) ) ;
#19563=DIRECTION ( 'NONE',  ( 0.01111468050521610164, -0.5103046645782707280, 0.8599218645824314722 ) ) ;
#19564=CARTESIAN_POINT ( 'NONE',  ( 58.87479767622038906, 143.5880916635284166, 105.9939182712553105 ) ) ;
#19576=EDGE_LOOP ( 'NONE', ( #12987, #15028, #21533, #11848 ) ) ;
#19578=CARTESIAN_POINT ( 'NONE',  ( 45.44350069997184249, 168.6907664596096765, 34.02200722522287180 ) ) ;
#19580=ORIENTED_EDGE ( 'NONE', *, *, #1103, .T. ) ;
#19605=DIRECTION ( 'NONE',  ( -7.125109674364534776E-05, 0.9999848031710252272, -0.005512562950849704026 ) ) ;
#19614=LINE ( 'NONE', #1717, #16205 ) ;
#19646=DIRECTION ( 'NONE',  ( -0.9999164797902015955, -2.045733645417851681E-15, 0.01292414190464156835 ) ) ;
#19674=VERTEX_POINT ( 'NONE', #20724 ) ;
#19687=LINE ( 'NONE', #1796, #13350 ) ;
#19707=CIRCLE ( 'NONE', #18632, 3.399999999999986144 ) ;
#19716=ORIENTED_EDGE ( 'NONE', *, *, #1952, .F. ) ;
#19727=CARTESIAN_POINT ( 'NONE',  ( 50.34270678259964882, 126.1473026246199254, 26.19146026598277643 ) ) ;
#19728=CARTESIAN_POINT ( 'NONE',  ( 68.31397436809166379, 127.4153035195791119, 255.9758934117053570 ) ) ;
#19738=EDGE_LOOP ( 'NONE', ( #16495, #9317, #11495, #8038 ) ) ;
#19742=DIRECTION ( 'NONE',  ( 7.125109674364536131E-05, -0.9999848031710253382, 0.005512562950849705760 ) ) ;
#19756=CYLINDRICAL_SURFACE ( 'NONE', #10297, 2.499999999999988010 ) ;
#19770=EDGE_LOOP ( 'NONE', ( #6352, #5934, #8719, #18840 ) ) ;
#19771=CIRCLE ( 'NONE', #13929, 2.499999999999988010 ) ;
#19787=CARTESIAN_POINT ( 'NONE',  ( 48.02316444802085016, 166.7281037598372961, 233.7692061953857774 ) ) ;
#19795=DIRECTION ( 'NONE',  ( -0.01292394549866632963, -0.005513023399716958026, -0.9999012842304692006 ) ) ;
#19823=DIRECTION ( 'NONE',  ( 7.125109674364534776E-05, -0.9999848031710252272, 0.005512562950849704893 ) ) ;
#19826=AXIS2_PLACEMENT_3D ( 'NONE', #11883, #8307, #5929 ) ;
#19832=EDGE_LOOP ( 'NONE', ( #18847, #5199, #21370 ) ) ;
#19844=ORIENTED_EDGE ( 'NONE', *, *, #7546, .F. ) ;
#19849=ADVANCED_FACE ( 'NONE', ( #10955 ), #14085, .F. ) ;
#19879=CARTESIAN_POINT ( 'NONE',  ( 68.30941429790007646, 191.4143309225247549, 255.6230893828509352 ) ) ;
#19899=AXIS2_PLACEMENT_3D ( 'NONE', #8133, #2741, #15041 ) ;
#19931=EDGE_CURVE ( 'NONE', #13755, #17081, #513, .T. ) ;
#19934=VECTOR ( 'NONE', #15640, 1000.000000000000227 ) ;
#19942=CIRCLE ( 'NONE', #6389, 2.499999999999988010 ) ;
#19949=DIRECTION ( 'NONE',  ( -0.01292394549866632963, -0.005513023399716958026, -0.9999012842304692006 ) ) ;
#19961=FACE_OUTER_BOUND ( 'NONE', #13483, .T. ) ;
#19962=CARTESIAN_POINT ( 'NONE',  ( 23.31673526217817027, 141.4150907639734385, 256.4803039161023435 ) ) ;
#19964=LINE ( 'NONE', #4457, #13789 ) ;
#19968=VERTEX_POINT ( 'NONE', #21832 ) ;
#19995=ORIENTED_EDGE ( 'NONE', *, *, #1064, .T. ) ;
#20003=EDGE_CURVE ( 'NONE', #10714, #11266, #18145, .T. ) ;
#20059=ADVANCED_FACE ( 'NONE', ( #10251 ), #17263, .F. ) ;
#20073=ORIENTED_EDGE ( 'NONE', *, *, #15132, .F. ) ;
#20075=VECTOR ( 'NONE', #4931, 1000.000000000000114 ) ;
#20076=CARTESIAN_POINT ( 'NONE',  ( -56.89103422957282419, 143.2573102595449654, 47.48611753646095224 ) ) ;
#20087=PLANE ( 'NONE',  #16632 ) ;
#20108=CARTESIAN_POINT ( 'NONE',  ( 50.34271970654513950, 126.1473081376433214, 26.19246016726700788 ) ) ;
#20123=ORIENTED_EDGE ( 'NONE', *, *, #452, .T. ) ;
#20125=CYLINDRICAL_SURFACE ( 'NONE', #18729, 10.00000000000000000 ) ;
#20127=ORIENTED_EDGE ( 'NONE', *, *, #14353, .F. ) ;
#20134=AXIS2_PLACEMENT_3D ( 'NONE', #16111, #18054, #9530 ) ;
#20174=VERTEX_POINT ( 'NONE', #143 ) ;
#20186=DIRECTION ( 'NONE',  ( 7.125109674364534776E-05, -0.9999848031710252272, 0.005512562950849704893 ) ) ;
#20193=DIRECTION ( 'NONE',  ( 0.01111468050521610164, -0.5103046645782707280, 0.8599218645824314722 ) ) ;
#20217=ADVANCED_FACE ( 'NONE', ( #3356 ), #3471, .F. ) ;
#20230=CARTESIAN_POINT ( 'NONE',  ( 58.90710753996705762, 143.6018742220277318, 108.4936714818314840 ) ) ;
#20234=ORIENTED_EDGE ( 'NONE', *, *, #18229, .F. ) ;
#20236=DIRECTION ( 'NONE',  ( 7.125109674364536131E-05, -0.9999848031710253382, 0.005512562950849705760 ) ) ;
#20240=CARTESIAN_POINT ( 'NONE',  ( 48.02316444802085016, 166.7281037598372961, 233.7692061953857774 ) ) ;
#20257=AXIS2_PLACEMENT_3D ( 'NONE', #1670, #1886, #21063 ) ;
#20262=DIRECTION ( 'NONE',  ( 0.01292394549866729934, 0.005513023399719703226, 0.9999012842304692006 ) ) ;
#20294=DIRECTION ( 'NONE',  ( 0.01111468050521610164, -0.5103046645782707280, 0.8599218645824314722 ) ) ;
#20304=CARTESIAN_POINT ( 'NONE',  ( -46.67642080778155389, 127.4153035195788846, 257.4621697307391059 ) ) ;
#20305=AXIS2_PLACEMENT_3D ( 'NONE', #8515, #22063, #18748 ) ;
#20310=EDGE_CURVE ( 'NONE', #3219, #19439, #16241, .T. ) ;
#20315=VECTOR ( 'NONE', #1985, 999.9999999999998863 ) ;
#20345=VECTOR ( 'NONE', #13284, 1000.000000000000227 ) ;
#20428=EDGE_CURVE ( 'NONE', #4699, #18675, #13354, .T. ) ;
#20447=ADVANCED_FACE ( 'NONE', ( #21915 ), #15949, .F. ) ;
#20450=LINE ( 'NONE', #20230, #18659 ) ;
#20454=VECTOR ( 'NONE', #14833, 999.9999999999998863 ) ;
#20462=DIRECTION ( 'NONE',  ( -0.01292394549866632963, -0.005513023399716958026, -0.9999012842304692006 ) ) ;
#20466=DIRECTION ( 'NONE',  ( -0.01292394549866632963, -0.005513023399716958026, -0.9999012842304692006 ) ) ;
#20478=ORIENTED_EDGE ( 'NONE', *, *, #17994, .T. ) ;
#20506=VERTEX_POINT ( 'NONE', #8037 ) ;
#20535=CARTESIAN_POINT ( 'NONE',  ( 58.87479767622038906, 143.5880916635284166, 105.9939182712553105 ) ) ;
#20541=CARTESIAN_POINT ( 'NONE',  ( 58.90831880861169623, 126.6021325681202825, 108.5873850519959092 ) ) ;
#20557=CARTESIAN_POINT ( 'NONE',  ( -44.54898248114630377, 168.6907664596094776, 35.18517999664061335 ) ) ;
#20591=VECTOR ( 'NONE', #1525, 999.9999999999998863 ) ;
#20596=VERTEX_POINT ( 'NONE', #15840 ) ;
#20610=DIRECTION ( 'NONE',  ( -0.9999164797902015955, 0.000000000000000000, 0.01292414190464162733 ) ) ;
#20616=VERTEX_POINT ( 'NONE', #7300 ) ;
#20621=CIRCLE ( 'NONE', #20975, 2.499999999999988010 ) ;
#20633=AXIS2_PLACEMENT_3D ( 'NONE', #1300, #22485, #20676 ) ;
#20634=CYLINDRICAL_SURFACE ( 'NONE', #3405, 3.399999999999986144 ) ;
#20638=ORIENTED_EDGE ( 'NONE', *, *, #15872, .T. ) ;
#20642=CARTESIAN_POINT ( 'NONE',  ( -46.67741832313596717, 141.4150907639732679, 257.3849938494272465 ) ) ;
#20649=DIRECTION ( 'NONE',  ( 7.125109674364536131E-05, -0.9999848031710253382, 0.005512562950849705760 ) ) ;
#20659=LINE ( 'NONE', #11949, #14806 ) ;
#20673=CARTESIAN_POINT ( 'NONE',  ( -46.67741832313596717, 141.4150907639732679, 257.3849938494272465 ) ) ;
#20676=DIRECTION ( 'NONE',  ( 0.01292394549866738782, 0.005513023399720700692, 0.9999012842304693116 ) ) ;
#20690=DIRECTION ( 'NONE',  ( 7.125109674364536131E-05, -0.9999848031710253382, 0.005512562950849705760 ) ) ;
#20696=DIRECTION ( 'NONE',  ( 0.9999164797902015955, 0.000000000000000000, -0.01292414190463754553 ) ) ;
#20722=EDGE_CURVE ( 'NONE', #22035, #18467, #14683, .T. ) ;
#20724=CARTESIAN_POINT ( 'NONE',  ( -45.07718948873534970, 165.9786531560170033, 257.2288776738097908 ) ) ;
#20729=CONICAL_SURFACE ( 'NONE', #6445, 3.399999999999986144, 1.029744258676653201 ) ;
#20757=CARTESIAN_POINT ( 'NONE',  ( -41.67747345744867715, 165.9786531560170033, 257.1849355913340673 ) ) ;
#20758=CARTESIAN_POINT ( 'NONE',  ( 59.68375553853174154, 126.9329139721035489, 168.5814621058240732 ) ) ;
#20761=CARTESIAN_POINT ( 'NONE',  ( 23.31388521830841754, 181.4144828908144405, 256.2598013980683049 ) ) ;
#20765=ORIENTED_EDGE ( 'NONE', *, *, #15808, .T. ) ;
#20786=CYLINDRICAL_SURFACE ( 'NONE', #5323, 9.999999999999992895 ) ;
#20798=ORIENTED_EDGE ( 'NONE', *, *, #10185, .T. ) ;
#20803=PRODUCT_DEFINITION ( 'UNKNOWN', '', #1856, #3271 ) ;
#20805=ORIENTED_EDGE ( 'NONE', *, *, #1901, .F. ) ;
#20810=LINE ( 'NONE', #18867, #3559 ) ;
#20817=LINE ( 'NONE', #17066, #10334 ) ;
#20875=AXIS2_PLACEMENT_3D ( 'NONE', #1314, #6794, #4948 ) ;
#20882=CARTESIAN_POINT ( 'NONE',  ( 58.06826235119833512, 126.2437860471384568, 43.59380157701544789 ) ) ;
#20888=CARTESIAN_POINT ( 'NONE',  ( -56.11559749965279309, 143.5880916635282176, 107.4801945902891021 ) ) ;
#20895=LINE ( 'NONE', #9048, #11074 ) ;
#20918=ORIENTED_EDGE ( 'NONE', *, *, #8242, .T. ) ;
#20921=ORIENTED_EDGE ( 'NONE', *, *, #10128, .F. ) ;
#20922=ADVANCED_FACE ( 'NONE', ( #10169 ), #1452, .F. ) ;
#20948=DIRECTION ( 'NONE',  ( -0.01292394549866632963, -0.005513023399716958026, -0.9999012842304692006 ) ) ;
#20958=AXIS2_PLACEMENT_3D ( 'NONE', #1298, #18614, #6342 ) ;
#20963=CARTESIAN_POINT ( 'NONE',  ( 44.91100620407951993, 166.8507685304810764, 256.0609518519894436 ) ) ;
#20975=AXIS2_PLACEMENT_3D ( 'NONE', #8588, #16086, #5247 ) ;
#21015=DIRECTION ( 'NONE',  ( 0.9999164797902015955, 2.045733645417851681E-15, -0.01292414190464156835 ) ) ;
#21020=FACE_OUTER_BOUND ( 'NONE', #10634, .T. ) ;
#21032=ORIENTED_EDGE ( 'NONE', *, *, #10075, .F. ) ;
#21033=AXIS2_PLACEMENT_3D ( 'NONE', #8648, #5320, #3381 ) ;
#21040=EDGE_CURVE ( 'NONE', #12722, #17081, #2803, .T. ) ;
#21053=AXIS2_PLACEMENT_3D ( 'NONE', #6980, #3536, #10548 ) ;
#21063=DIRECTION ( 'NONE',  ( -0.01292394549866738782, -0.005513023399720700692, -0.9999012842304693116 ) ) ;
#21066=AXIS2_PLACEMENT_3D ( 'NONE', #3182, #15180, #21897 ) ;
#21067=CYLINDRICAL_SURFACE ( 'NONE', #21033, 2.499999999999988010 ) ;
#21102=VECTOR ( 'NONE', #9649, 1000.000000000000000 ) ;
#21149=ORIENTED_EDGE ( 'NONE', *, *, #10201, .F. ) ;
#21184=VECTOR ( 'NONE', #16912, 1000.000000000000000 ) ;
#21196=STYLED_ITEM ( 'NONE', ( #19247 ), #1836 ) ;
#21197=DIRECTION ( 'NONE',  ( 0.9999164797902015955, 0.000000000000000000, -0.01292414190463754553 ) ) ;
#21209=VECTOR ( 'NONE', #7627, 1000.000000000000000 ) ;
#21215=VERTEX_POINT ( 'NONE', #8204 ) ;
#21219=AXIS2_PLACEMENT_3D ( 'NONE', #22539, #18791, #10073 ) ;
#21226=FACE_OUTER_BOUND ( 'NONE', #15847, .T. ) ;
#21264=CARTESIAN_POINT ( 'NONE',  ( -9.009919365157752935, 180.4221386788646271, 76.66529449372310978 ) ) ;
#21278=CARTESIAN_POINT ( 'NONE',  ( -56.85872436582616274, 143.2710928180442522, 49.98587074703711153 ) ) ;
#21294=EDGE_CURVE ( 'NONE', #6357, #8826, #6215, .T. ) ;
#21330=ORIENTED_EDGE ( 'NONE', *, *, #21294, .T. ) ;
#21338=EDGE_LOOP ( 'NONE', ( #9570, #17929 ) ) ;
#21342=AXIS2_PLACEMENT_3D ( 'NONE', #2795, #11748, #1312 ) ;
#21354=EDGE_LOOP ( 'NONE', ( #12654, #11428, #1837, #9238 ) ) ;
#21358=VECTOR ( 'NONE', #17122, 999.9999999999998863 ) ;
#21370=ORIENTED_EDGE ( 'NONE', *, *, #1414, .T. ) ;
#21398=CARTESIAN_POINT ( 'NONE',  ( -56.08328763590613164, 143.6018742220275044, 109.9799478008652471 ) ) ;
#21404=EDGE_CURVE ( 'NONE', #18381, #16056, #14985, .T. ) ;
#21450=EDGE_CURVE ( 'NONE', #8826, #12812, #4828, .T. ) ;
#21469=EDGE_CURVE ( 'NONE', #4209, #530, #6680, .T. ) ;
#21533=ORIENTED_EDGE ( 'NONE', *, *, #11174, .T. ) ;
#21565=LINE ( 'NONE', #5840, #17980 ) ;
#21570=ORIENTED_EDGE ( 'NONE', *, *, #4125, .F. ) ;
#21586=AXIS2_PLACEMENT_3D ( 'NONE', #19564, #14082, #5319 ) ;
#21589=ORIENTED_EDGE ( 'NONE', *, *, #14157, .T. ) ;
#21602=CIRCLE ( 'NONE', #9153, 2.499999999999988010 ) ;
#21639=CARTESIAN_POINT ( 'NONE',  ( -9.007069321288007302, 140.4227465520236251, 76.88579701175710568 ) ) ;
#21668=CARTESIAN_POINT ( 'NONE',  ( -46.67642080778155389, 127.4153035195788846, 257.4621697307391059 ) ) ;
#21674=CARTESIAN_POINT ( 'NONE',  ( 58.87600894486503478, 126.5883500096209815, 106.0876318414197499 ) ) ;
#21694=CARTESIAN_POINT ( 'NONE',  ( 1.828589379190189046, 190.7803332315567388, 141.4745109201486457 ) ) ;
#21708=PLANE ( 'NONE',  #15534 ) ;
#21715=ORIENTED_EDGE ( 'NONE', *, *, #22408, .F. ) ;
#21743=AXIS2_PLACEMENT_3D ( 'NONE', #22534, #6502, #18785 ) ;
#21746=AXIS2_PLACEMENT_3D ( 'NONE', #6475, #22504, #20462 ) ;
#21750=ORIENTED_EDGE ( 'NONE', *, *, #13731, .F. ) ;
#21758=AXIS2_PLACEMENT_3D ( 'NONE', #3548, #10343, #8599 ) ;
#21768=VECTOR ( 'NONE', #773, 999.9999999999998863 ) ;
#21775=DIRECTION ( 'NONE',  ( 7.125109674364534776E-05, -0.9999848031710252272, 0.005512562950849704893 ) ) ;
#21792=DIRECTION ( 'NONE',  ( 0.01292394549866738782, 0.005513023399720700692, 0.9999012842304693116 ) ) ;
#21795=ORIENTED_EDGE ( 'NONE', *, *, #10299, .F. ) ;
#21809=FACE_OUTER_BOUND ( 'NONE', #11779, .T. ) ;
#21810=CARTESIAN_POINT ( 'NONE',  ( -56.92334409331949274, 143.2435277010456787, 44.98636432588479295 ) ) ;
#21816=ORIENTED_EDGE ( 'NONE', *, *, #15289, .T. ) ;
#21832=CARTESIAN_POINT ( 'NONE',  ( 53.31422965588423324, 141.4150907639734953, 256.0925796589630181 ) ) ;
#21897=DIRECTION ( 'NONE',  ( -0.9999164797902015955, 0.000000000000000000, 0.01292414190464162733 ) ) ;
#21914=AXIS2_PLACEMENT_3D ( 'NONE', #1335, #22422, #4638 ) ;
#21915=FACE_OUTER_BOUND ( 'NONE', #6491, .T. ) ;
#21955=DIRECTION ( 'NONE',  ( 0.9999164797902017066, 0.000000000000000000, -0.01292414190463751951 ) ) ;
#21999=ORIENTED_EDGE ( 'NONE', *, *, #18153, .F. ) ;
#22006=VECTOR ( 'NONE', #17505, 999.9999999999998863 ) ;
#22012=EDGE_CURVE ( 'NONE', #18467, #11266, #19614, .T. ) ;
#22020=ORIENTED_EDGE ( 'NONE', *, *, #798, .F. ) ;
#22035=VERTEX_POINT ( 'NONE', #3884 ) ;
#22048=CARTESIAN_POINT ( 'NONE',  ( 45.75746115295205385, 168.8246939296725202, 58.31253523502198988 ) ) ;
#22051=FACE_OUTER_BOUND ( 'NONE', #2663, .T. ) ;
#22058=CONICAL_SURFACE ( 'NONE', #4099, 3.399999999999986144, 1.029744258676653201 ) ;
#22063=DIRECTION ( 'NONE',  ( 7.125109674364534776E-05, -0.9999848031710252272, 0.005512562950849704893 ) ) ;
#22069=EDGE_LOOP ( 'NONE', ( #1696, #2862, #483, #10056 ) ) ;
#22071=AXIS2_PLACEMENT_3D ( 'NONE', #10221, #17224, #1719 ) ;
#22077=ADVANCED_FACE ( 'NONE', ( #10896 ), #17699, .F. ) ;
#22094=CARTESIAN_POINT ( 'NONE',  ( -56.14790736339946164, 143.5743091050289024, 104.9804413797129286 ) ) ;
#22107=EDGE_CURVE ( 'NONE', #16756, #10313, #10793, .T. ) ;
#22110=EDGE_LOOP ( 'NONE', ( #10720, #2162, #20765, #17850 ) ) ;
#22128=CARTESIAN_POINT ( 'NONE',  ( -38.56531521350735403, 165.8559883853732515, 234.8931899347302874 ) ) ;
#22137=DIRECTION ( 'NONE',  ( -0.01292394549866738782, -0.005513023399720700692, -0.9999012842304693116 ) ) ;
#22141=EDGE_LOOP ( 'NONE', ( #8018, #14667, #8768 ) ) ;
#22153=ADVANCED_FACE ( 'NONE', ( #16296 ), #765, .F. ) ;
#22158=CARTESIAN_POINT ( 'NONE',  ( 68.31397436809166379, 127.4153035195791119, 255.9758934117053570 ) ) ;
#22162=ORIENTED_EDGE ( 'NONE', *, *, #9360, .T. ) ;
#22190=CARTESIAN_POINT ( 'NONE',  ( 65.33690683320658366, 190.1463355405889786, 25.64579400984300150 ) ) ;
#22229=LINE ( 'NONE', #18810, #9904 ) ;
#22232=CIRCLE ( 'NONE', #12376, 3.399999999999986144 ) ;
#22260=CARTESIAN_POINT ( 'NONE',  ( -40.86170866251428180, 168.8134312302532862, 57.38904148829276863 ) ) ;
#22286=ORIENTED_EDGE ( 'NONE', *, *, #8992, .T. ) ;
#22289=CARTESIAN_POINT ( 'NONE',  ( 58.13167081004702652, 143.2710928180444796, 48.49959442800331999 ) ) ;
#22319=VERTEX_POINT ( 'NONE', #4867 ) ;
#22328=DIRECTION ( 'NONE',  ( -0.9999164797902015955, 0.000000000000000000, 0.01292414190464162733 ) ) ;
#22344=CARTESIAN_POINT ( 'NONE',  ( -56.89103422957282419, 143.2573102595449654, 47.48611753646095224 ) ) ;
#22359=FACE_OUTER_BOUND ( 'NONE', #12425, .T. ) ;
#22367=AXIS2_PLACEMENT_3D ( 'NONE', #17573, #3951, #19795 ) ;
#22382=VECTOR ( 'NONE', #13162, 999.9999999999998863 ) ;
#22400=EDGE_LOOP ( 'NONE', ( #8346, #4746 ) ) ;
#22402=CARTESIAN_POINT ( 'NONE',  ( -55.34016076973275489, 143.9188730675114414, 167.4742716441172377 ) ) ;
#22408=EDGE_CURVE ( 'NONE', #11384, #3194, #5399, .T. ) ;
#22411=CARTESIAN_POINT ( 'NONE',  ( -56.08207636726148593, 126.6021325681200551, 110.0736613710297007 ) ) ;
#22422=DIRECTION ( 'NONE',  ( 0.01292394549866738608, 0.005513023399720699824, 0.9999012842304692006 ) ) ;
#22437=AXIS2_PLACEMENT_3D ( 'NONE', #20535, #6868, #17464 ) ;
#22450=DIRECTION ( 'NONE',  ( 0.01292394549866738782, 0.005513023399720701559, 0.9999012842304693116 ) ) ;
#22458=DIRECTION ( 'NONE',  ( 0.9999164797902017066, 0.000000000000000000, -0.01292414190463751951 ) ) ;
#22467=AXIS2_PLACEMENT_3D ( 'NONE', #13954, #180, #19230 ) ;
#22473=ORIENTED_EDGE ( 'NONE', *, *, #14588, .T. ) ;
#22480=ORIENTED_EDGE ( 'NONE', *, *, #13782, .T. ) ;
#22483=LINE ( 'NONE', #18724, #21184 ) ;
#22485=DIRECTION ( 'NONE',  ( -7.125109674364536131E-05, 0.9999848031710253382, -0.005512562950849706628 ) ) ;
#22486=AXIS2_PLACEMENT_3D ( 'NONE', #10588, #5063, #14281 ) ;
#22504=DIRECTION ( 'NONE',  ( 7.125109674364534776E-05, -0.9999848031710252272, 0.005512562950849704893 ) ) ;
#22521=ORIENTED_EDGE ( 'NONE', *, *, #7546, .T. ) ;
#22534=CARTESIAN_POINT ( 'NONE',  ( -19.00623411919002592, 140.4227465520235967, 77.01503843080352851 ) ) ;
#22539=CARTESIAN_POINT ( 'NONE',  ( -41.96503124479402658, 165.8559883853732515, 234.9371320172060678 ) ) ;
#22614=CARTESIAN_POINT ( 'NONE',  ( 65.34011313256004883, 145.1470193978928478, 25.89385934263124867 ) ) ;
#22628=CARTESIAN_POINT ( 'NONE',  ( 65.44350469654938252, 145.1911235850906223, 33.89306961647502447 ) ) ;
#22643=CARTESIAN_POINT ( 'NONE',  ( -56.92334409331949274, 143.2435277010456787, 44.98636432588477874 ) ) ;
#22664=DIRECTION ( 'NONE',  ( 0.01292394549866738608, 0.005513023399720698957, 0.9999012842304692006 ) ) ;
ENDSEC;
END-ISO-10303-21;
